ISO-10303-21;
HEADER;
/* Generated by software containing ST-Developer
 * from STEP Tools, Inc. (www.steptools.com) 
 */

FILE_DESCRIPTION(
/* description */ ('Wheel Holder-Mirrored'),
/* implementation_level */ '2;1');

FILE_NAME(
/* name */ 'Hex flange bolt small M6x1.00 x 25.step',
/* time_stamp */ '2026-10-07T09:01:46-07:00',
/* author */ (''),
/* organization */ (''),
/* preprocessor_version */ 'ST-DEVELOPER v20.2',
/* originating_system */ 'Autodesk Translation Framework v15.15.0.0',
/* authorisation */ '');

FILE_SCHEMA (('AUTOMOTIVE_DESIGN { 1 0 10303 214 3 1 1 }'));
ENDSEC;

DATA;
#10=MECHANICAL_DESIGN_GEOMETRIC_PRESENTATION_REPRESENTATION('',(#201),#3832);
#78=(
BOUNDED_SURFACE()
B_SPLINE_SURFACE(3,2,((#2888,#2889,#2890),(#2891,#2892,#2893),(#2894,#2895,
#2896),(#2897,#2898,#2899),(#2900,#2901,#2902)),.UNSPECIFIED.,.F.,.F.,.F.)
B_SPLINE_SURFACE_WITH_KNOTS((4,1,4),(3,3),(0.0199905421078539,0.0227092821601536,
0.0254280222134474),(0.,1.00056005679341),.UNSPECIFIED.)
GEOMETRIC_REPRESENTATION_ITEM()
RATIONAL_B_SPLINE_SURFACE(((1.,0.802854637372621,1.00022082519925),(1.,
0.81108958019377,1.00021160112791),(1.,0.82690910145913,1.00019388146721),
(1.,0.811291833393597,1.00021137458136),(1.,0.802795753782992,1.00022089115557)))
REPRESENTATION_ITEM('')
SURFACE()
);
#79=(
BOUNDED_SURFACE()
B_SPLINE_SURFACE(3,2,((#2927,#2928,#2929),(#2930,#2931,#2932),(#2933,#2934,
#2935),(#2936,#2937,#2938),(#2939,#2940,#2941)),.UNSPECIFIED.,.F.,.F.,.F.)
B_SPLINE_SURFACE_WITH_KNOTS((4,1,4),(3,3),(0.0199863987269074,0.0227063701116868,
0.0254263415355543),(0.,1.00056355085534),.UNSPECIFIED.)
GEOMETRIC_REPRESENTATION_ITEM()
RATIONAL_B_SPLINE_SURFACE(((1.,0.802841957060873,1.00022221716746),(1.,
0.811080854660757,1.00021293109189),(1.,0.826916200792063,1.00019508304617),
(1.,0.811283787847418,1.00021270236556),(1.,0.802782519169589,1.00022228416001)))
REPRESENTATION_ITEM('')
SURFACE()
);
#80=(
BOUNDED_SURFACE()
B_SPLINE_SURFACE(3,2,((#2954,#2955,#2956),(#2957,#2958,#2959),(#2960,#2961,
#2962),(#2963,#2964,#2965),(#2966,#2967,#2968)),.UNSPECIFIED.,.F.,.F.,.F.)
B_SPLINE_SURFACE_WITH_KNOTS((4,1,4),(3,3),(0.0199905421079487,0.0227092821601536,
0.0254280222133526),(0.,1.00056005680003),.UNSPECIFIED.)
GEOMETRIC_REPRESENTATION_ITEM()
RATIONAL_B_SPLINE_SURFACE(((1.,0.802854637372034,1.00022082520187),(1.,
0.811089580193672,1.00021160113042),(1.,0.826909101456828,1.00019388146951),
(1.,0.81129183339351,1.00021137458386),(1.,0.802795753782428,1.00022089115817)))
REPRESENTATION_ITEM('')
SURFACE()
);
#81=(
BOUNDED_SURFACE()
B_SPLINE_SURFACE(3,2,((#2981,#2982,#2983),(#2984,#2985,#2986),(#2987,#2988,
#2989),(#2990,#2991,#2992),(#2993,#2994,#2995)),.UNSPECIFIED.,.F.,.F.,.F.)
B_SPLINE_SURFACE_WITH_KNOTS((4,1,4),(3,3),(0.0199905421080522,0.0227092821601536,
0.0254280222132491),(0.,1.00056005679973),.UNSPECIFIED.)
GEOMETRIC_REPRESENTATION_ITEM()
RATIONAL_B_SPLINE_SURFACE(((1.,0.802854637372995,1.00022082520174),(1.,
0.811089580194489,1.00021160113031),(1.,0.826909101456198,1.0001938814694),
(1.,0.811291833394166,1.00021137458374),(1.,0.802795753783457,1.00022089115806)))
REPRESENTATION_ITEM('')
SURFACE()
);
#82=(
BOUNDED_SURFACE()
B_SPLINE_SURFACE(3,2,((#3008,#3009,#3010),(#3011,#3012,#3013),(#3014,#3015,
#3016),(#3017,#3018,#3019),(#3020,#3021,#3022)),.UNSPECIFIED.,.F.,.F.,.F.)
B_SPLINE_SURFACE_WITH_KNOTS((4,1,4),(3,3),(0.019994704332767,0.022712204724463,
0.0254297050789377),(0.,1.00055654499458),.UNSPECIFIED.)
GEOMETRIC_REPRESENTATION_ITEM()
RATIONAL_B_SPLINE_SURFACE(((1.,0.802867397371381,1.00021942632651),(1.,
0.811098353635701,1.00021026453151),(1.,0.826901960236561,1.00019267369521),
(1.,0.811299927383003,1.00021004016178),(1.,0.802809067580306,1.00021949125283)))
REPRESENTATION_ITEM('')
SURFACE()
);
#83=(
BOUNDED_SURFACE()
B_SPLINE_SURFACE(3,2,((#3035,#3036,#3037),(#3038,#3039,#3040),(#3041,#3042,
#3043),(#3044,#3045,#3046),(#3047,#3048,#3049)),.UNSPECIFIED.,.F.,.F.,.F.)
B_SPLINE_SURFACE_WITH_KNOTS((4,1,4),(3,3),(0.0199905421078943,0.0227092821601536,
0.025428022213407),(0.,1.00056005680679),.UNSPECIFIED.)
GEOMETRIC_REPRESENTATION_ITEM()
RATIONAL_B_SPLINE_SURFACE(((1.,0.802854637370352,1.00022082520454),(1.,
0.811089580191479,1.00021160113298),(1.,0.826909101456581,1.00019388147184),
(1.,0.811291833391307,1.00021137458641),(1.,0.802795753780734,1.00022089116085)))
REPRESENTATION_ITEM('')
SURFACE()
);
#90=TOROIDAL_SURFACE('',#1935,0.0068,0.000567100162269167);
#91=TOROIDAL_SURFACE('',#1948,0.00325,0.00025);
#93=CONICAL_SURFACE('',#1922,0.004,1.0471975511966);
#94=CONICAL_SURFACE('',#1924,0.004,1.0471975511966);
#95=CONICAL_SURFACE('',#1926,0.004,1.0471975511966);
#96=CONICAL_SURFACE('',#1928,0.004,1.0471975511966);
#97=CONICAL_SURFACE('',#1930,0.004,1.0471975511966);
#98=CONICAL_SURFACE('',#1932,0.004,1.0471975511966);
#99=CONICAL_SURFACE('',#1940,1.,1.22173047639603);
#100=CONICAL_SURFACE('',#1950,0.002458734125,0.78539816339745);
#110=(
BOUNDED_CURVE()
B_SPLINE_CURVE(2,(#2688,#2689,#2690),.UNSPECIFIED.,.F.,.F.)
B_SPLINE_CURVE_WITH_KNOTS((3,3),(0.899640233852609,1.41204223156836),
 .UNSPECIFIED.)
CURVE()
GEOMETRIC_REPRESENTATION_ITEM()
RATIONAL_B_SPLINE_CURVE((2.04103265936813,2.19890708499154,2.19890708499154))
REPRESENTATION_ITEM('')
);
#111=(
BOUNDED_CURVE()
B_SPLINE_CURVE(2,(#2691,#2692,#2693),.UNSPECIFIED.,.F.,.F.)
B_SPLINE_CURVE_WITH_KNOTS((3,3),(1.41204223156836,1.92444422930209),
 .UNSPECIFIED.)
CURVE()
GEOMETRIC_REPRESENTATION_ITEM()
RATIONAL_B_SPLINE_CURVE((2.19890708499154,2.19890708499154,2.04103265935705))
REPRESENTATION_ITEM('')
);
#112=(
BOUNDED_CURVE()
B_SPLINE_CURVE(2,(#2715,#2716,#2717),.UNSPECIFIED.,.F.,.F.)
B_SPLINE_CURVE_WITH_KNOTS((3,3),(0.899640233852608,1.41204223156835),
 .UNSPECIFIED.)
CURVE()
GEOMETRIC_REPRESENTATION_ITEM()
RATIONAL_B_SPLINE_CURVE((2.04103265936813,2.19890708499154,2.19890708499154))
REPRESENTATION_ITEM('')
);
#113=(
BOUNDED_CURVE()
B_SPLINE_CURVE(2,(#2718,#2719,#2720),.UNSPECIFIED.,.F.,.F.)
B_SPLINE_CURVE_WITH_KNOTS((3,3),(1.41204223156835,1.9244442293021),
 .UNSPECIFIED.)
CURVE()
GEOMETRIC_REPRESENTATION_ITEM()
RATIONAL_B_SPLINE_CURVE((2.19890708499154,2.19890708499154,2.04103265935704))
REPRESENTATION_ITEM('')
);
#114=(
BOUNDED_CURVE()
B_SPLINE_CURVE(2,(#2742,#2743,#2744),.UNSPECIFIED.,.F.,.F.)
B_SPLINE_CURVE_WITH_KNOTS((3,3),(-1.41204232189231,-0.899640300628516),
 .UNSPECIFIED.)
CURVE()
GEOMETRIC_REPRESENTATION_ITEM()
RATIONAL_B_SPLINE_CURVE((2.19890717995419,2.19890717995419,2.04103274751277))
REPRESENTATION_ITEM('')
);
#115=(
BOUNDED_CURVE()
B_SPLINE_CURVE(2,(#2745,#2746,#2747),.UNSPECIFIED.,.F.,.F.)
B_SPLINE_CURVE_WITH_KNOTS((3,3),(-1.9244443431741,-1.41204232189231),
 .UNSPECIFIED.)
CURVE()
GEOMETRIC_REPRESENTATION_ITEM()
RATIONAL_B_SPLINE_CURVE((2.04103274750169,2.19890717995419,2.19890717995419))
REPRESENTATION_ITEM('')
);
#116=(
BOUNDED_CURVE()
B_SPLINE_CURVE(2,(#2769,#2770,#2771),.UNSPECIFIED.,.F.,.F.)
B_SPLINE_CURVE_WITH_KNOTS((3,3),(0.899640233852631,1.41204223156839),
 .UNSPECIFIED.)
CURVE()
GEOMETRIC_REPRESENTATION_ITEM()
RATIONAL_B_SPLINE_CURVE((2.04103265936816,2.19890708499158,2.19890708499158))
REPRESENTATION_ITEM('')
);
#117=(
BOUNDED_CURVE()
B_SPLINE_CURVE(2,(#2772,#2773,#2774),.UNSPECIFIED.,.F.,.F.)
B_SPLINE_CURVE_WITH_KNOTS((3,3),(1.41204223156839,1.92444422930213),
 .UNSPECIFIED.)
CURVE()
GEOMETRIC_REPRESENTATION_ITEM()
RATIONAL_B_SPLINE_CURVE((2.19890708499158,2.19890708499158,2.04103265935708))
REPRESENTATION_ITEM('')
);
#118=(
BOUNDED_CURVE()
B_SPLINE_CURVE(2,(#2796,#2797,#2798),.UNSPECIFIED.,.F.,.F.)
B_SPLINE_CURVE_WITH_KNOTS((3,3),(0.899640233852618,1.41204223156836),
 .UNSPECIFIED.)
CURVE()
GEOMETRIC_REPRESENTATION_ITEM()
RATIONAL_B_SPLINE_CURVE((2.04103265936815,2.19890708499156,2.19890708499156))
REPRESENTATION_ITEM('')
);
#119=(
BOUNDED_CURVE()
B_SPLINE_CURVE(2,(#2799,#2800,#2801),.UNSPECIFIED.,.F.,.F.)
B_SPLINE_CURVE_WITH_KNOTS((3,3),(1.41204223156836,1.92444422930211),
 .UNSPECIFIED.)
CURVE()
GEOMETRIC_REPRESENTATION_ITEM()
RATIONAL_B_SPLINE_CURVE((2.19890708499156,2.19890708499156,2.04103265935706))
REPRESENTATION_ITEM('')
);
#120=(
BOUNDED_CURVE()
B_SPLINE_CURVE(2,(#2820,#2821,#2822),.UNSPECIFIED.,.F.,.F.)
B_SPLINE_CURVE_WITH_KNOTS((3,3),(0.899640166945249,1.4120421410666),
 .UNSPECIFIED.)
CURVE()
GEOMETRIC_REPRESENTATION_ITEM()
RATIONAL_B_SPLINE_CURVE((2.04103257104998,2.19890698984196,2.19890698984195))
REPRESENTATION_ITEM('')
);
#121=(
BOUNDED_CURVE()
B_SPLINE_CURVE(2,(#2823,#2824,#2825),.UNSPECIFIED.,.F.,.F.)
B_SPLINE_CURVE_WITH_KNOTS((3,3),(1.4120421410666,1.92444411520593),
 .UNSPECIFIED.)
CURVE()
GEOMETRIC_REPRESENTATION_ITEM()
RATIONAL_B_SPLINE_CURVE((2.19890698984195,2.19890698984195,2.04103257103889))
REPRESENTATION_ITEM('')
);
#134=B_SPLINE_CURVE_WITH_KNOTS('',3,(#2669,#2670,#2671,#2672,#2673,#2674,
#2675,#2676,#2677,#2678,#2679,#2680,#2681,#2682,#2683,#2684),
 .UNSPECIFIED.,.F.,.F.,(4,3,3,3,3,4),(0.,0.00115933810312788,0.0023008628112466,
0.00231867620625576,0.00347801430938363,0.00463735241251151),
 .UNSPECIFIED.);
#135=B_SPLINE_CURVE_WITH_KNOTS('',3,(#2696,#2697,#2698,#2699,#2700,#2701,
#2702,#2703,#2704,#2705,#2706,#2707,#2708,#2709,#2710,#2711),
 .UNSPECIFIED.,.F.,.F.,(4,3,3,3,3,4),(1.55309542619116E-19,0.00115933810312788,
0.0023008628112466,0.00231867620625576,0.00347801430938364,0.00463735241251152),
 .UNSPECIFIED.);
#136=B_SPLINE_CURVE_WITH_KNOTS('',3,(#2723,#2724,#2725,#2726,#2727,#2728,
#2729,#2730,#2731,#2732,#2733,#2734,#2735,#2736,#2737,#2738),
 .UNSPECIFIED.,.F.,.F.,(4,3,3,3,3,4),(0.,0.00115932447661246,0.00230074676248248,
0.00231864895322491,0.00347797342983737,0.00463729790644982),
 .UNSPECIFIED.);
#137=B_SPLINE_CURVE_WITH_KNOTS('',3,(#2750,#2751,#2752,#2753,#2754,#2755,
#2756,#2757,#2758,#2759,#2760,#2761,#2762,#2763,#2764,#2765),
 .UNSPECIFIED.,.F.,.F.,(4,3,3,3,3,4),(0.,0.00115933810312788,0.0023008628112466,
0.00231867620625576,0.00347801430938363,0.00463735241251151),
 .UNSPECIFIED.);
#138=B_SPLINE_CURVE_WITH_KNOTS('',3,(#2777,#2778,#2779,#2780,#2781,#2782,
#2783,#2784,#2785,#2786,#2787,#2788,#2789,#2790,#2791,#2792),
 .UNSPECIFIED.,.F.,.F.,(4,3,3,3,3,4),(3.24894099173316E-19,0.00115933810312788,
0.0023008628112466,0.00231867620625576,0.00347801430938364,0.00463735241251152),
 .UNSPECIFIED.);
#139=B_SPLINE_CURVE_WITH_KNOTS('',3,(#2803,#2804,#2805,#2806,#2807,#2808,
#2809,#2810,#2811,#2812,#2813,#2814,#2815,#2816,#2817,#2818),
 .UNSPECIFIED.,.F.,.F.,(4,3,3,3,3,4),(0.,0.00115935174734299,0.00230097898664969,
0.00231870349468598,0.00347805524202897,0.00463740698937197),
 .UNSPECIFIED.);
#140=B_SPLINE_CURVE_WITH_KNOTS('',3,(#2851,#2852,#2853,#2854,#2855),
 .UNSPECIFIED.,.F.,.F.,(4,1,4),(0.,0.00248123639135078,0.00496246810726153),
 .UNSPECIFIED.);
#141=B_SPLINE_CURVE_WITH_KNOTS('',3,(#2857,#2858,#2859,#2860,#2861),
 .UNSPECIFIED.,.F.,.F.,(4,1,4),(0.,0.00248125883902994,0.00496251282372695),
 .UNSPECIFIED.);
#142=B_SPLINE_CURVE_WITH_KNOTS('',3,(#2863,#2864,#2865,#2866,#2867),
 .UNSPECIFIED.,.F.,.F.,(4,1,4),(0.,0.00248123639135078,0.00496246796815217),
 .UNSPECIFIED.);
#143=B_SPLINE_CURVE_WITH_KNOTS('',3,(#2869,#2870,#2871,#2872,#2873),
 .UNSPECIFIED.,.F.,.F.,(4,1,4),(0.,0.00248123639135079,0.00496246818443855),
 .UNSPECIFIED.);
#144=B_SPLINE_CURVE_WITH_KNOTS('',3,(#2875,#2876,#2877,#2878,#2879),
 .UNSPECIFIED.,.F.,.F.,(4,1,4),(0.,0.00248121396259867,0.00496242332668108),
 .UNSPECIFIED.);
#145=B_SPLINE_CURVE_WITH_KNOTS('',3,(#2880,#2881,#2882,#2883,#2884),
 .UNSPECIFIED.,.F.,.F.,(4,1,4),(0.,0.00248123639135079,0.00496246828961979),
 .UNSPECIFIED.);
#146=B_SPLINE_CURVE_WITH_KNOTS('',3,(#2903,#2904,#2905,#2906,#2907,#2908,
#2909,#2910,#2911,#2912,#2913,#2914),.UNSPECIFIED.,.F.,.F.,(4,2,2,2,2,4),
(-0.0536945210860223,-0.0408448591087579,-0.026670772721852,-0.0132475634127344,
0.,0.00261482960537117),.UNSPECIFIED.);
#147=B_SPLINE_CURVE_WITH_KNOTS('',3,(#2915,#2916,#2917,#2918,#2919,#2920,
#2921,#2922,#2923,#2924,#2925,#2926),.UNSPECIFIED.,.F.,.F.,(4,2,2,2,2,4),
(-0.0536943501278373,-0.0408447644220054,-0.0266707574515382,-0.0132475635493419,
0.,0.0026147568848072),.UNSPECIFIED.);
#148=B_SPLINE_CURVE_WITH_KNOTS('',3,(#2942,#2943,#2944,#2945,#2946,#2947,
#2948,#2949,#2950,#2951,#2952,#2953),.UNSPECIFIED.,.F.,.F.,(4,2,2,2,2,4),
(0.,0.0128045620123767,0.0269286898692442,0.0403044328139677,0.0535040873424465,
0.0561132593100496),.UNSPECIFIED.);
#149=B_SPLINE_CURVE_WITH_KNOTS('',3,(#2969,#2970,#2971,#2972,#2973,#2974,
#2975,#2976,#2977,#2978,#2979,#2980),.UNSPECIFIED.,.F.,.F.,(4,2,2,2,2,4),
(-0.0536946737885314,-0.0408450041369318,-0.0266709101282734,-0.0132476284737636,
0.,0.00261482249258708),.UNSPECIFIED.);
#150=B_SPLINE_CURVE_WITH_KNOTS('',3,(#2996,#2997,#2998,#2999,#3000,#3001,
#3002,#3003,#3004,#3005,#3006,#3007),.UNSPECIFIED.,.F.,.F.,(4,2,2,2,2,4),
(0.,0.0128045651857744,0.0269286883548746,0.0403044491788003,0.0535041176088484,
0.0561132658579917),.UNSPECIFIED.);
#151=B_SPLINE_CURVE_WITH_KNOTS('',3,(#3023,#3024,#3025,#3026,#3027,#3028,
#3029,#3030,#3031,#3032,#3033,#3034),.UNSPECIFIED.,.F.,.F.,(4,2,2,2,2,4),
(0.,0.012804574182279,0.0269287091649782,0.0403044718863404,0.0535041388980146,
0.0561134038245879),.UNSPECIFIED.);
#189=SHAPE_REPRESENTATION_RELATIONSHIP('SRR','None',#3866,#195);
#195=ADVANCED_BREP_SHAPE_REPRESENTATION('',(#207),#3829);
#201=STYLED_ITEM('',(#3905),#207);
#207=MANIFOLD_SOLID_BREP('Body1',#1786);
#224=FACE_BOUND('',#436,.T.);
#243=PLANE('',#1916);
#244=PLANE('',#1917);
#245=PLANE('',#1918);
#246=PLANE('',#1919);
#247=PLANE('',#1920);
#248=PLANE('',#1921);
#249=PLANE('',#1934);
#250=PLANE('',#1941);
#251=PLANE('',#1946);
#302=FACE_OUTER_BOUND('',#420,.T.);
#303=FACE_OUTER_BOUND('',#421,.T.);
#304=FACE_OUTER_BOUND('',#422,.T.);
#305=FACE_OUTER_BOUND('',#423,.T.);
#306=FACE_OUTER_BOUND('',#424,.T.);
#307=FACE_OUTER_BOUND('',#425,.T.);
#308=FACE_OUTER_BOUND('',#426,.T.);
#309=FACE_OUTER_BOUND('',#427,.T.);
#310=FACE_OUTER_BOUND('',#428,.T.);
#311=FACE_OUTER_BOUND('',#429,.T.);
#312=FACE_OUTER_BOUND('',#430,.T.);
#313=FACE_OUTER_BOUND('',#431,.T.);
#314=FACE_OUTER_BOUND('',#432,.T.);
#315=FACE_OUTER_BOUND('',#433,.T.);
#316=FACE_OUTER_BOUND('',#434,.T.);
#317=FACE_OUTER_BOUND('',#435,.T.);
#318=FACE_OUTER_BOUND('',#437,.T.);
#319=FACE_OUTER_BOUND('',#438,.T.);
#320=FACE_OUTER_BOUND('',#439,.T.);
#321=FACE_OUTER_BOUND('',#440,.T.);
#322=FACE_OUTER_BOUND('',#441,.T.);
#323=FACE_OUTER_BOUND('',#442,.T.);
#324=FACE_OUTER_BOUND('',#443,.T.);
#325=FACE_OUTER_BOUND('',#444,.T.);
#326=FACE_OUTER_BOUND('',#445,.T.);
#327=FACE_OUTER_BOUND('',#446,.T.);
#420=EDGE_LOOP('',(#1279,#1280,#1281,#1282,#1283));
#421=EDGE_LOOP('',(#1284,#1285,#1286,#1287,#1288));
#422=EDGE_LOOP('',(#1289,#1290,#1291,#1292,#1293));
#423=EDGE_LOOP('',(#1294,#1295,#1296,#1297,#1298));
#424=EDGE_LOOP('',(#1299,#1300,#1301,#1302,#1303));
#425=EDGE_LOOP('',(#1304,#1305,#1306,#1307,#1308));
#426=EDGE_LOOP('',(#1309,#1310,#1311));
#427=EDGE_LOOP('',(#1312,#1313,#1314));
#428=EDGE_LOOP('',(#1315,#1316,#1317));
#429=EDGE_LOOP('',(#1318,#1319,#1320));
#430=EDGE_LOOP('',(#1321,#1322,#1323));
#431=EDGE_LOOP('',(#1324,#1325,#1326));
#432=EDGE_LOOP('',(#1327,#1328,#1329,#1330,#1331,#1332));
#433=EDGE_LOOP('',(#1333,#1334,#1335,#1336,#1337));
#434=EDGE_LOOP('',(#1338,#1339,#1340,#1341,#1342,#1343,#1344,#1345,#1346,
#1347));
#435=EDGE_LOOP('',(#1348));
#436=EDGE_LOOP('',(#1349));
#437=EDGE_LOOP('',(#1350,#1351,#1352,#1353));
#438=EDGE_LOOP('',(#1354,#1355,#1356,#1357));
#439=EDGE_LOOP('',(#1358,#1359,#1360,#1361));
#440=EDGE_LOOP('',(#1362,#1363,#1364,#1365));
#441=EDGE_LOOP('',(#1366,#1367,#1368,#1369));
#442=EDGE_LOOP('',(#1370,#1371,#1372,#1373));
#443=EDGE_LOOP('',(#1374,#1375,#1376,#1377));
#444=EDGE_LOOP('',(#1378));
#445=EDGE_LOOP('',(#1379,#1380,#1381,#1382));
#446=EDGE_LOOP('',(#1383,#1384,#1385,#1386));
#535=LINE('',#2667,#628);
#536=LINE('',#2686,#629);
#537=LINE('',#2713,#630);
#538=LINE('',#2740,#631);
#539=LINE('',#2767,#632);
#540=LINE('',#2794,#633);
#541=LINE('',#2849,#634);
#542=LINE('',#3054,#635);
#543=LINE('',#3062,#636);
#628=VECTOR('',#2207,1.);
#629=VECTOR('',#2208,1.);
#630=VECTOR('',#2211,1.);
#631=VECTOR('',#2214,1.);
#632=VECTOR('',#2217,1.);
#633=VECTOR('',#2220,1.);
#634=VECTOR('',#2261,1.);
#635=VECTOR('',#2270,0.003);
#636=VECTOR('',#2283,0.002458734125);
#710=CIRCLE('',#1923,0.004);
#711=CIRCLE('',#1925,0.004);
#712=CIRCLE('',#1927,0.004);
#713=CIRCLE('',#1929,0.004);
#714=CIRCLE('',#1931,0.004);
#715=CIRCLE('',#1933,0.004);
#716=CIRCLE('',#1936,0.00699395967877932);
#717=CIRCLE('',#1937,0.00699395967877932);
#718=CIRCLE('',#1938,0.000567100162269167);
#719=CIRCLE('',#1939,0.0068);
#720=CIRCLE('',#1942,0.00325);
#721=CIRCLE('',#1944,0.003);
#722=CIRCLE('',#1945,0.003);
#723=CIRCLE('',#1947,0.002458734125);
#724=CIRCLE('',#1949,0.00025);
#788=VERTEX_POINT('',#2665);
#789=VERTEX_POINT('',#2666);
#790=VERTEX_POINT('',#2668);
#791=VERTEX_POINT('',#2685);
#792=VERTEX_POINT('',#2687);
#793=VERTEX_POINT('',#2695);
#794=VERTEX_POINT('',#2712);
#795=VERTEX_POINT('',#2714);
#796=VERTEX_POINT('',#2722);
#797=VERTEX_POINT('',#2739);
#798=VERTEX_POINT('',#2741);
#799=VERTEX_POINT('',#2749);
#800=VERTEX_POINT('',#2766);
#801=VERTEX_POINT('',#2768);
#802=VERTEX_POINT('',#2776);
#803=VERTEX_POINT('',#2793);
#804=VERTEX_POINT('',#2795);
#805=VERTEX_POINT('',#2819);
#806=VERTEX_POINT('',#2840);
#807=VERTEX_POINT('',#2841);
#808=VERTEX_POINT('',#2844);
#809=VERTEX_POINT('',#2848);
#810=VERTEX_POINT('',#2850);
#811=VERTEX_POINT('',#2856);
#812=VERTEX_POINT('',#2862);
#813=VERTEX_POINT('',#2868);
#814=VERTEX_POINT('',#2874);
#815=VERTEX_POINT('',#2886);
#816=VERTEX_POINT('',#3051);
#817=VERTEX_POINT('',#3053);
#818=VERTEX_POINT('',#3057);
#966=EDGE_CURVE('',#788,#789,#535,.T.);
#967=EDGE_CURVE('',#789,#790,#134,.T.);
#968=EDGE_CURVE('',#791,#790,#536,.T.);
#969=EDGE_CURVE('',#791,#792,#110,.T.);
#970=EDGE_CURVE('',#792,#788,#111,.T.);
#971=EDGE_CURVE('',#790,#793,#135,.T.);
#972=EDGE_CURVE('',#794,#793,#537,.T.);
#973=EDGE_CURVE('',#794,#795,#112,.T.);
#974=EDGE_CURVE('',#795,#791,#113,.T.);
#975=EDGE_CURVE('',#793,#796,#136,.T.);
#976=EDGE_CURVE('',#797,#796,#538,.T.);
#977=EDGE_CURVE('',#797,#798,#114,.F.);
#978=EDGE_CURVE('',#798,#794,#115,.F.);
#979=EDGE_CURVE('',#796,#799,#137,.T.);
#980=EDGE_CURVE('',#800,#799,#539,.T.);
#981=EDGE_CURVE('',#800,#801,#116,.T.);
#982=EDGE_CURVE('',#801,#797,#117,.T.);
#983=EDGE_CURVE('',#799,#802,#138,.T.);
#984=EDGE_CURVE('',#803,#802,#540,.T.);
#985=EDGE_CURVE('',#803,#804,#118,.T.);
#986=EDGE_CURVE('',#804,#800,#119,.T.);
#987=EDGE_CURVE('',#802,#789,#139,.T.);
#988=EDGE_CURVE('',#788,#805,#120,.T.);
#989=EDGE_CURVE('',#805,#803,#121,.T.);
#990=EDGE_CURVE('',#804,#805,#710,.T.);
#991=EDGE_CURVE('',#805,#792,#711,.T.);
#992=EDGE_CURVE('',#801,#804,#712,.T.);
#993=EDGE_CURVE('',#798,#801,#713,.T.);
#994=EDGE_CURVE('',#795,#798,#714,.T.);
#995=EDGE_CURVE('',#792,#795,#715,.T.);
#996=EDGE_CURVE('',#806,#807,#716,.T.);
#997=EDGE_CURVE('',#807,#806,#717,.T.);
#998=EDGE_CURVE('',#807,#808,#718,.T.);
#999=EDGE_CURVE('',#808,#808,#719,.T.);
#1000=EDGE_CURVE('',#806,#809,#541,.T.);
#1001=EDGE_CURVE('',#809,#810,#140,.T.);
#1002=EDGE_CURVE('',#810,#811,#141,.T.);
#1003=EDGE_CURVE('',#811,#812,#142,.T.);
#1004=EDGE_CURVE('',#812,#813,#143,.T.);
#1005=EDGE_CURVE('',#813,#814,#144,.T.);
#1006=EDGE_CURVE('',#814,#809,#145,.T.);
#1007=EDGE_CURVE('',#815,#815,#720,.T.);
#1008=EDGE_CURVE('',#799,#809,#146,.T.);
#1009=EDGE_CURVE('',#810,#796,#147,.F.);
#1010=EDGE_CURVE('',#811,#793,#148,.F.);
#1011=EDGE_CURVE('',#802,#814,#149,.T.);
#1012=EDGE_CURVE('',#812,#790,#150,.F.);
#1013=EDGE_CURVE('',#789,#813,#151,.T.);
#1014=EDGE_CURVE('',#816,#816,#721,.F.);
#1015=EDGE_CURVE('',#816,#817,#542,.T.);
#1016=EDGE_CURVE('',#817,#817,#722,.F.);
#1017=EDGE_CURVE('',#818,#818,#723,.T.);
#1018=EDGE_CURVE('',#815,#816,#724,.T.);
#1019=EDGE_CURVE('',#817,#818,#543,.T.);
#1279=ORIENTED_EDGE('',*,*,#966,.T.);
#1280=ORIENTED_EDGE('',*,*,#967,.T.);
#1281=ORIENTED_EDGE('',*,*,#968,.F.);
#1282=ORIENTED_EDGE('',*,*,#969,.T.);
#1283=ORIENTED_EDGE('',*,*,#970,.T.);
#1284=ORIENTED_EDGE('',*,*,#968,.T.);
#1285=ORIENTED_EDGE('',*,*,#971,.T.);
#1286=ORIENTED_EDGE('',*,*,#972,.F.);
#1287=ORIENTED_EDGE('',*,*,#973,.T.);
#1288=ORIENTED_EDGE('',*,*,#974,.T.);
#1289=ORIENTED_EDGE('',*,*,#972,.T.);
#1290=ORIENTED_EDGE('',*,*,#975,.T.);
#1291=ORIENTED_EDGE('',*,*,#976,.F.);
#1292=ORIENTED_EDGE('',*,*,#977,.T.);
#1293=ORIENTED_EDGE('',*,*,#978,.T.);
#1294=ORIENTED_EDGE('',*,*,#976,.T.);
#1295=ORIENTED_EDGE('',*,*,#979,.T.);
#1296=ORIENTED_EDGE('',*,*,#980,.F.);
#1297=ORIENTED_EDGE('',*,*,#981,.T.);
#1298=ORIENTED_EDGE('',*,*,#982,.T.);
#1299=ORIENTED_EDGE('',*,*,#980,.T.);
#1300=ORIENTED_EDGE('',*,*,#983,.T.);
#1301=ORIENTED_EDGE('',*,*,#984,.F.);
#1302=ORIENTED_EDGE('',*,*,#985,.T.);
#1303=ORIENTED_EDGE('',*,*,#986,.T.);
#1304=ORIENTED_EDGE('',*,*,#984,.T.);
#1305=ORIENTED_EDGE('',*,*,#987,.T.);
#1306=ORIENTED_EDGE('',*,*,#966,.F.);
#1307=ORIENTED_EDGE('',*,*,#988,.T.);
#1308=ORIENTED_EDGE('',*,*,#989,.T.);
#1309=ORIENTED_EDGE('',*,*,#989,.F.);
#1310=ORIENTED_EDGE('',*,*,#990,.F.);
#1311=ORIENTED_EDGE('',*,*,#985,.F.);
#1312=ORIENTED_EDGE('',*,*,#991,.F.);
#1313=ORIENTED_EDGE('',*,*,#988,.F.);
#1314=ORIENTED_EDGE('',*,*,#970,.F.);
#1315=ORIENTED_EDGE('',*,*,#986,.F.);
#1316=ORIENTED_EDGE('',*,*,#992,.F.);
#1317=ORIENTED_EDGE('',*,*,#981,.F.);
#1318=ORIENTED_EDGE('',*,*,#982,.F.);
#1319=ORIENTED_EDGE('',*,*,#993,.F.);
#1320=ORIENTED_EDGE('',*,*,#977,.F.);
#1321=ORIENTED_EDGE('',*,*,#994,.F.);
#1322=ORIENTED_EDGE('',*,*,#973,.F.);
#1323=ORIENTED_EDGE('',*,*,#978,.F.);
#1324=ORIENTED_EDGE('',*,*,#995,.F.);
#1325=ORIENTED_EDGE('',*,*,#969,.F.);
#1326=ORIENTED_EDGE('',*,*,#974,.F.);
#1327=ORIENTED_EDGE('',*,*,#992,.T.);
#1328=ORIENTED_EDGE('',*,*,#990,.T.);
#1329=ORIENTED_EDGE('',*,*,#991,.T.);
#1330=ORIENTED_EDGE('',*,*,#995,.T.);
#1331=ORIENTED_EDGE('',*,*,#994,.T.);
#1332=ORIENTED_EDGE('',*,*,#993,.T.);
#1333=ORIENTED_EDGE('',*,*,#996,.F.);
#1334=ORIENTED_EDGE('',*,*,#997,.F.);
#1335=ORIENTED_EDGE('',*,*,#998,.T.);
#1336=ORIENTED_EDGE('',*,*,#999,.T.);
#1337=ORIENTED_EDGE('',*,*,#998,.F.);
#1338=ORIENTED_EDGE('',*,*,#996,.T.);
#1339=ORIENTED_EDGE('',*,*,#997,.T.);
#1340=ORIENTED_EDGE('',*,*,#1000,.T.);
#1341=ORIENTED_EDGE('',*,*,#1001,.T.);
#1342=ORIENTED_EDGE('',*,*,#1002,.T.);
#1343=ORIENTED_EDGE('',*,*,#1003,.T.);
#1344=ORIENTED_EDGE('',*,*,#1004,.T.);
#1345=ORIENTED_EDGE('',*,*,#1005,.T.);
#1346=ORIENTED_EDGE('',*,*,#1006,.T.);
#1347=ORIENTED_EDGE('',*,*,#1000,.F.);
#1348=ORIENTED_EDGE('',*,*,#999,.F.);
#1349=ORIENTED_EDGE('',*,*,#1007,.T.);
#1350=ORIENTED_EDGE('',*,*,#1008,.F.);
#1351=ORIENTED_EDGE('',*,*,#979,.F.);
#1352=ORIENTED_EDGE('',*,*,#1009,.F.);
#1353=ORIENTED_EDGE('',*,*,#1001,.F.);
#1354=ORIENTED_EDGE('',*,*,#1009,.T.);
#1355=ORIENTED_EDGE('',*,*,#975,.F.);
#1356=ORIENTED_EDGE('',*,*,#1010,.F.);
#1357=ORIENTED_EDGE('',*,*,#1002,.F.);
#1358=ORIENTED_EDGE('',*,*,#1008,.T.);
#1359=ORIENTED_EDGE('',*,*,#1006,.F.);
#1360=ORIENTED_EDGE('',*,*,#1011,.F.);
#1361=ORIENTED_EDGE('',*,*,#983,.F.);
#1362=ORIENTED_EDGE('',*,*,#1010,.T.);
#1363=ORIENTED_EDGE('',*,*,#971,.F.);
#1364=ORIENTED_EDGE('',*,*,#1012,.F.);
#1365=ORIENTED_EDGE('',*,*,#1003,.F.);
#1366=ORIENTED_EDGE('',*,*,#1011,.T.);
#1367=ORIENTED_EDGE('',*,*,#1005,.F.);
#1368=ORIENTED_EDGE('',*,*,#1013,.F.);
#1369=ORIENTED_EDGE('',*,*,#987,.F.);
#1370=ORIENTED_EDGE('',*,*,#1012,.T.);
#1371=ORIENTED_EDGE('',*,*,#967,.F.);
#1372=ORIENTED_EDGE('',*,*,#1013,.T.);
#1373=ORIENTED_EDGE('',*,*,#1004,.F.);
#1374=ORIENTED_EDGE('',*,*,#1014,.T.);
#1375=ORIENTED_EDGE('',*,*,#1015,.T.);
#1376=ORIENTED_EDGE('',*,*,#1016,.T.);
#1377=ORIENTED_EDGE('',*,*,#1015,.F.);
#1378=ORIENTED_EDGE('',*,*,#1017,.T.);
#1379=ORIENTED_EDGE('',*,*,#1007,.F.);
#1380=ORIENTED_EDGE('',*,*,#1018,.T.);
#1381=ORIENTED_EDGE('',*,*,#1014,.F.);
#1382=ORIENTED_EDGE('',*,*,#1018,.F.);
#1383=ORIENTED_EDGE('',*,*,#1016,.F.);
#1384=ORIENTED_EDGE('',*,*,#1019,.T.);
#1385=ORIENTED_EDGE('',*,*,#1017,.F.);
#1386=ORIENTED_EDGE('',*,*,#1019,.F.);
#1666=CYLINDRICAL_SURFACE('',#1943,0.003);
#1708=ADVANCED_FACE('',(#302),#243,.T.);
#1709=ADVANCED_FACE('',(#303),#244,.T.);
#1710=ADVANCED_FACE('',(#304),#245,.T.);
#1711=ADVANCED_FACE('',(#305),#246,.T.);
#1712=ADVANCED_FACE('',(#306),#247,.T.);
#1713=ADVANCED_FACE('',(#307),#248,.T.);
#1714=ADVANCED_FACE('',(#308),#93,.T.);
#1715=ADVANCED_FACE('',(#309),#94,.T.);
#1716=ADVANCED_FACE('',(#310),#95,.T.);
#1717=ADVANCED_FACE('',(#311),#96,.T.);
#1718=ADVANCED_FACE('',(#312),#97,.T.);
#1719=ADVANCED_FACE('',(#313),#98,.T.);
#1720=ADVANCED_FACE('',(#314),#249,.T.);
#1721=ADVANCED_FACE('',(#315),#90,.T.);
#1722=ADVANCED_FACE('',(#316),#99,.T.);
#1723=ADVANCED_FACE('',(#317,#224),#250,.F.);
#1724=ADVANCED_FACE('',(#318),#78,.F.);
#1725=ADVANCED_FACE('',(#319),#79,.F.);
#1726=ADVANCED_FACE('',(#320),#80,.F.);
#1727=ADVANCED_FACE('',(#321),#81,.F.);
#1728=ADVANCED_FACE('',(#322),#82,.F.);
#1729=ADVANCED_FACE('',(#323),#83,.F.);
#1730=ADVANCED_FACE('',(#324),#1666,.T.);
#1731=ADVANCED_FACE('',(#325),#251,.T.);
#1732=ADVANCED_FACE('',(#326),#91,.F.);
#1733=ADVANCED_FACE('',(#327),#100,.T.);
#1786=CLOSED_SHELL('',(#1708,#1709,#1710,#1711,#1712,#1713,#1714,#1715,
#1716,#1717,#1718,#1719,#1720,#1721,#1722,#1723,#1724,#1725,#1726,#1727,
#1728,#1729,#1730,#1731,#1732,#1733));
#1915=AXIS2_PLACEMENT_3D('',#2663,#2203,#2204);
#1916=AXIS2_PLACEMENT_3D('',#2664,#2205,#2206);
#1917=AXIS2_PLACEMENT_3D('',#2694,#2209,#2210);
#1918=AXIS2_PLACEMENT_3D('',#2721,#2212,#2213);
#1919=AXIS2_PLACEMENT_3D('',#2748,#2215,#2216);
#1920=AXIS2_PLACEMENT_3D('',#2775,#2218,#2219);
#1921=AXIS2_PLACEMENT_3D('',#2802,#2221,#2222);
#1922=AXIS2_PLACEMENT_3D('',#2826,#2223,#2224);
#1923=AXIS2_PLACEMENT_3D('',#2827,#2225,#2226);
#1924=AXIS2_PLACEMENT_3D('',#2828,#2227,#2228);
#1925=AXIS2_PLACEMENT_3D('',#2829,#2229,#2230);
#1926=AXIS2_PLACEMENT_3D('',#2830,#2231,#2232);
#1927=AXIS2_PLACEMENT_3D('',#2831,#2233,#2234);
#1928=AXIS2_PLACEMENT_3D('',#2832,#2235,#2236);
#1929=AXIS2_PLACEMENT_3D('',#2833,#2237,#2238);
#1930=AXIS2_PLACEMENT_3D('',#2834,#2239,#2240);
#1931=AXIS2_PLACEMENT_3D('',#2835,#2241,#2242);
#1932=AXIS2_PLACEMENT_3D('',#2836,#2243,#2244);
#1933=AXIS2_PLACEMENT_3D('',#2837,#2245,#2246);
#1934=AXIS2_PLACEMENT_3D('',#2838,#2247,#2248);
#1935=AXIS2_PLACEMENT_3D('',#2839,#2249,#2250);
#1936=AXIS2_PLACEMENT_3D('',#2842,#2251,#2252);
#1937=AXIS2_PLACEMENT_3D('',#2843,#2253,#2254);
#1938=AXIS2_PLACEMENT_3D('',#2845,#2255,#2256);
#1939=AXIS2_PLACEMENT_3D('',#2846,#2257,#2258);
#1940=AXIS2_PLACEMENT_3D('',#2847,#2259,#2260);
#1941=AXIS2_PLACEMENT_3D('',#2885,#2262,#2263);
#1942=AXIS2_PLACEMENT_3D('',#2887,#2264,#2265);
#1943=AXIS2_PLACEMENT_3D('',#3050,#2266,#2267);
#1944=AXIS2_PLACEMENT_3D('',#3052,#2268,#2269);
#1945=AXIS2_PLACEMENT_3D('',#3055,#2271,#2272);
#1946=AXIS2_PLACEMENT_3D('',#3056,#2273,#2274);
#1947=AXIS2_PLACEMENT_3D('',#3058,#2275,#2276);
#1948=AXIS2_PLACEMENT_3D('',#3059,#2277,#2278);
#1949=AXIS2_PLACEMENT_3D('',#3060,#2279,#2280);
#1950=AXIS2_PLACEMENT_3D('',#3061,#2281,#2282);
#2203=DIRECTION('axis',(0.,0.,1.));
#2204=DIRECTION('refdir',(1.,0.,0.));
#2205=DIRECTION('center_axis',(-0.866025403784439,0.5,0.));
#2206=DIRECTION('ref_axis',(-0.5,-0.866025403784439,0.));
#2207=DIRECTION('',(0.,0.,-1.));
#2208=DIRECTION('',(0.,0.,-1.));
#2209=DIRECTION('center_axis',(-0.866025403784438,-0.5,0.));
#2210=DIRECTION('ref_axis',(0.5,-0.866025403784438,0.));
#2211=DIRECTION('',(0.,0.,-1.));
#2212=DIRECTION('center_axis',(0.,-1.,0.));
#2213=DIRECTION('ref_axis',(0.,0.,-1.));
#2214=DIRECTION('',(0.,0.,-1.));
#2215=DIRECTION('center_axis',(0.866025403784439,-0.5,0.));
#2216=DIRECTION('ref_axis',(0.5,0.866025403784439,0.));
#2217=DIRECTION('',(0.,0.,-1.));
#2218=DIRECTION('center_axis',(0.866025403784438,0.5,0.));
#2219=DIRECTION('ref_axis',(-0.5,0.866025403784438,0.));
#2220=DIRECTION('',(0.,0.,-1.));
#2221=DIRECTION('center_axis',(0.,1.,0.));
#2222=DIRECTION('ref_axis',(0.,0.,1.));
#2223=DIRECTION('center_axis',(0.,0.,-1.));
#2224=DIRECTION('ref_axis',(-1.,0.,0.));
#2225=DIRECTION('center_axis',(0.,0.,1.));
#2226=DIRECTION('ref_axis',(1.,0.,0.));
#2227=DIRECTION('center_axis',(0.,0.,-1.));
#2228=DIRECTION('ref_axis',(-1.,0.,0.));
#2229=DIRECTION('center_axis',(0.,0.,1.));
#2230=DIRECTION('ref_axis',(1.,0.,0.));
#2231=DIRECTION('center_axis',(0.,0.,-1.));
#2232=DIRECTION('ref_axis',(1.,1.22464679914735E-16,0.));
#2233=DIRECTION('center_axis',(0.,0.,1.));
#2234=DIRECTION('ref_axis',(1.,0.,0.));
#2235=DIRECTION('center_axis',(0.,0.,-1.));
#2236=DIRECTION('ref_axis',(-1.,0.,0.));
#2237=DIRECTION('center_axis',(0.,0.,1.));
#2238=DIRECTION('ref_axis',(1.,0.,0.));
#2239=DIRECTION('center_axis',(0.,0.,-1.));
#2240=DIRECTION('ref_axis',(-1.,0.,0.));
#2241=DIRECTION('center_axis',(0.,0.,1.));
#2242=DIRECTION('ref_axis',(1.,0.,0.));
#2243=DIRECTION('center_axis',(0.,0.,-1.));
#2244=DIRECTION('ref_axis',(-1.,0.,0.));
#2245=DIRECTION('center_axis',(0.,0.,1.));
#2246=DIRECTION('ref_axis',(1.,0.,0.));
#2247=DIRECTION('center_axis',(0.,0.,1.));
#2248=DIRECTION('ref_axis',(1.,0.,0.));
#2249=DIRECTION('center_axis',(0.,0.,1.));
#2250=DIRECTION('ref_axis',(1.,0.,0.));
#2251=DIRECTION('center_axis',(0.,0.,1.));
#2252=DIRECTION('ref_axis',(1.,0.,0.));
#2253=DIRECTION('center_axis',(0.,0.,1.));
#2254=DIRECTION('ref_axis',(1.,0.,0.));
#2255=DIRECTION('center_axis',(1.22464679914735E-16,-1.,0.));
#2256=DIRECTION('ref_axis',(-1.,-1.22464679914735E-16,0.));
#2257=DIRECTION('center_axis',(0.,0.,1.));
#2258=DIRECTION('ref_axis',(1.,0.,0.));
#2259=DIRECTION('center_axis',(0.,0.,-1.));
#2260=DIRECTION('ref_axis',(-1.,0.,0.));
#2261=DIRECTION('',(-0.939692620785908,1.15079156022785E-16,0.342020143325669));
#2262=DIRECTION('center_axis',(0.,0.,1.));
#2263=DIRECTION('ref_axis',(1.,0.,0.));
#2264=DIRECTION('center_axis',(0.,0.,1.));
#2265=DIRECTION('ref_axis',(1.,0.,0.));
#2266=DIRECTION('center_axis',(0.,0.,1.));
#2267=DIRECTION('ref_axis',(1.,0.,0.));
#2268=DIRECTION('center_axis',(0.,0.,1.));
#2269=DIRECTION('ref_axis',(1.,0.,0.));
#2270=DIRECTION('',(0.,0.,-1.));
#2271=DIRECTION('center_axis',(0.,0.,-1.));
#2272=DIRECTION('ref_axis',(-1.,0.,0.));
#2273=DIRECTION('center_axis',(0.,0.,-1.));
#2274=DIRECTION('ref_axis',(1.,0.,0.));
#2275=DIRECTION('center_axis',(0.,0.,-1.));
#2276=DIRECTION('ref_axis',(-1.,0.,0.));
#2277=DIRECTION('center_axis',(0.,0.,1.));
#2278=DIRECTION('ref_axis',(1.,0.,0.));
#2279=DIRECTION('center_axis',(-1.22464679914735E-16,1.,0.));
#2280=DIRECTION('ref_axis',(-1.,-1.22464679914735E-16,0.));
#2281=DIRECTION('center_axis',(0.,0.,1.));
#2282=DIRECTION('ref_axis',(1.,0.,0.));
#2283=DIRECTION('',(0.707106781186549,8.65956056235495E-17,-0.707106781186546));
#2663=CARTESIAN_POINT('',(0.,0.,0.));
#2664=CARTESIAN_POINT('Origin',(-0.00346410161513775,0.002,0.0068));
#2665=CARTESIAN_POINT('',(-0.00230940107675851,0.004,0.00644273441009184));
#2666=CARTESIAN_POINT('',(-0.00230939436406612,0.00399999494215664,0.0022625182008993));
#2667=CARTESIAN_POINT('',(-0.00230940107675851,0.004,0.0068));
#2668=CARTESIAN_POINT('',(-0.00461879440075555,3.31248999445318E-9,0.00226251801022537));
#2669=CARTESIAN_POINT('Ctrl Pts',(-0.00230940691705295,0.00399998988431329,
0.00226254053913407));
#2670=CARTESIAN_POINT('Ctrl Pts',(-0.00250052112625622,0.00366897036392486,
0.00232700363594611));
#2671=CARTESIAN_POINT('Ctrl Pts',(-0.00269262130445346,0.003336243093075,
0.0023789007474104));
#2672=CARTESIAN_POINT('Ctrl Pts',(-0.00288523530706997,0.00300262585845459,
0.00241461216933165));
#2673=CARTESIAN_POINT('Ctrl Pts',(-0.00307488976811388,0.00267413470014111,
0.00244977488017086));
#2674=CARTESIAN_POINT('Ctrl Pts',(-0.00326504319652788,0.00234477935046048,
0.00246919460122286));
#2675=CARTESIAN_POINT('Ctrl Pts',(-0.00345519948963801,0.00201541895392153,
0.00246969208645218));
#2676=CARTESIAN_POINT('Ctrl Pts',(-0.00345816686225689,0.00201027931322677,
0.00246969984966645));
#2677=CARTESIAN_POINT('Ctrl Pts',(-0.00346113423804048,0.00200513966704103,
0.00246970300391286));
#2678=CARTESIAN_POINT('Ctrl Pts',(-0.00346410161390816,0.00200000002070232,
0.00246970156489889));
#2679=CARTESIAN_POINT('Ctrl Pts',(-0.00365722549107684,0.00166549961614694,
0.00246960791044814));
#2680=CARTESIAN_POINT('Ctrl Pts',(-0.00385033581825397,0.00133102273658184,
0.0024498267811737));
#2681=CARTESIAN_POINT('Ctrl Pts',(-0.00404294431061013,0.000997415041851726,
0.00241413900952665));
#2682=CARTESIAN_POINT('Ctrl Pts',(-0.00423555280296629,0.000663807347121617,
0.00237845123787961));
#2683=CARTESIAN_POINT('Ctrl Pts',(-0.00442766851201852,0.000331053178111033,
0.00232683813848012));
#2684=CARTESIAN_POINT('Ctrl Pts',(-0.00461879248828856,1.67406667220262E-8,
0.00226249548131684));
#2685=CARTESIAN_POINT('',(-0.00461880215351701,8.67361737988403E-19,0.00644273441009184));
#2686=CARTESIAN_POINT('',(-0.00461880215351701,4.33680868994202E-19,0.0068));
#2687=CARTESIAN_POINT('',(-0.00346410161513775,0.002,0.0068));
#2688=CARTESIAN_POINT('Ctrl Pts',(-0.00461880215350316,2.39844418489033E-14,
0.00644273441009984));
#2689=CARTESIAN_POINT('Ctrl Pts',(-0.00399999999999443,0.00107179676973413,
0.0068));
#2690=CARTESIAN_POINT('Ctrl Pts',(-0.00346410161513775,0.00199999999999999,
0.0068));
#2691=CARTESIAN_POINT('Ctrl Pts',(-0.00346410161513775,0.00199999999999999,
0.0068));
#2692=CARTESIAN_POINT('Ctrl Pts',(-0.00292820323026226,0.00292820323029845,
0.0068));
#2693=CARTESIAN_POINT('Ctrl Pts',(-0.00230940107672554,0.00400000000005709,
0.00644273441007281));
#2694=CARTESIAN_POINT('Origin',(-0.00346410161513775,-0.002,0.0068));
#2695=CARTESIAN_POINT('',(-0.00230940010168572,-0.00399999162966664,0.00226251820212234));
#2696=CARTESIAN_POINT('Ctrl Pts',(-0.00461879631322255,-1.01156867331198E-8,
0.0022625405391339));
#2697=CARTESIAN_POINT('Ctrl Pts',(-0.00442768210401926,-0.000331029636075182,
0.00232700363594575));
#2698=CARTESIAN_POINT('Ctrl Pts',(-0.00423558192403004,-0.000663756905890421,
0.00237890074741006));
#2699=CARTESIAN_POINT('Ctrl Pts',(-0.00404296792501672,-0.000997374142591104,
0.00241461216933148));
#2700=CARTESIAN_POINT('Ctrl Pts',(-0.00385331346752063,-0.0013258653029529,
0.00244977488017086));
#2701=CARTESIAN_POINT('Ctrl Pts',(-0.00366316008203189,-0.00165522067741645,
0.00246919460122286));
#2702=CARTESIAN_POINT('Ctrl Pts',(-0.00347300375818371,-0.00198458105620877,
0.00246969208645221));
#2703=CARTESIAN_POINT('Ctrl Pts',(-0.00347003638508517,-0.0019897206966266,
0.00246969984966648));
#2704=CARTESIAN_POINT('Ctrl Pts',(-0.00346706900881365,-0.00199486034253063,
0.00246970300391289));
#2705=CARTESIAN_POINT('Ctrl Pts',(-0.0034641016324517,-0.00199999998858397,
0.00246970156489892));
#2706=CARTESIAN_POINT('Ctrl Pts',(-0.0032709777231149,-0.00233450037456709,
0.0024696079104482));
#2707=CARTESIAN_POINT('Ctrl Pts',(-0.00307786741202155,-0.00266897726341815,
0.00244982678117377));
#2708=CARTESIAN_POINT('Ctrl Pts',(-0.00288525891966538,-0.00300258495814827,
0.00241413900952672));
#2709=CARTESIAN_POINT('Ctrl Pts',(-0.00269265042730922,-0.00333619265287839,
0.00237845123787968));
#2710=CARTESIAN_POINT('Ctrl Pts',(-0.00250053471825699,-0.00366894682188897,
0.00232683813848018));
#2711=CARTESIAN_POINT('Ctrl Pts',(-0.00230941074198694,-0.00399998325933328,
0.00226249548131687));
#2712=CARTESIAN_POINT('',(-0.00230940107675851,-0.004,0.00644273441009184));
#2713=CARTESIAN_POINT('',(-0.0023094010767585,-0.004,0.0068));
#2714=CARTESIAN_POINT('',(-0.00346410161513775,-0.002,0.0068));
#2715=CARTESIAN_POINT('Ctrl Pts',(-0.00230940107677235,-0.003999999999976,
0.00644273441009984));
#2716=CARTESIAN_POINT('Ctrl Pts',(-0.00292820323028107,-0.00292820323026586,
0.0068));
#2717=CARTESIAN_POINT('Ctrl Pts',(-0.00346410161513775,-0.002,0.0068));
#2718=CARTESIAN_POINT('Ctrl Pts',(-0.00346410161513775,-0.002,0.0068));
#2719=CARTESIAN_POINT('Ctrl Pts',(-0.00400000000001325,-0.00107179676970153,
0.0068));
#2720=CARTESIAN_POINT('Ctrl Pts',(-0.00461880215354998,5.71219321355913E-14,
0.0064427344100728));
#2721=CARTESIAN_POINT('Origin',(1.86807858924195E-18,-0.004,0.0068));
#2722=CARTESIAN_POINT('',(0.00230939429934915,-0.00399999494215665,0.00226251781990864));
#2723=CARTESIAN_POINT('Ctrl Pts',(-0.0023093894613845,-0.004,0.00226254092292782));
#2724=CARTESIAN_POINT('Ctrl Pts',(-0.00192716228032193,-0.004,0.00232700487022803));
#2725=CARTESIAN_POINT('Ctrl Pts',(-0.00154296885754916,-0.00399999999884996,
0.00237890343398045));
#2726=CARTESIAN_POINT('Ctrl Pts',(-0.00115774723711367,-0.00400000000116236,
0.002414613419996));
#2727=CARTESIAN_POINT('Ctrl Pts',(-0.000778474176435409,-0.00400000000343905,
0.00244977197542076));
#2728=CARTESIAN_POINT('Ctrl Pts',(-0.000398203312159713,-0.00400000002845795,
0.00246919150443257));
#2729=CARTESIAN_POINT('Ctrl Pts',(-1.79205700010576E-5,-0.00400000001033966,
0.00246969098913674));
#2730=CARTESIAN_POINT('Ctrl Pts',(-1.19561742901489E-5,-0.00400000001005549,
0.00246969882310893));
#2731=CARTESIAN_POINT('Ctrl Pts',(-5.99177071537931E-6,-0.00400000000976655,
0.00246970200182142));
#2732=CARTESIAN_POINT('Ctrl Pts',(-2.7365606690663E-8,-0.00400000000947396,
0.002469700541216));
#2733=CARTESIAN_POINT('Ctrl Pts',(0.000386220380851912,-0.00399999999052638,
0.00246960595415449));
#2734=CARTESIAN_POINT('Ctrl Pts',(0.000772447112493431,-0.004,0.00244982367082224));
#2735=CARTESIAN_POINT('Ctrl Pts',(0.00115767059475419,-0.004,0.00241413610794756));
#2736=CARTESIAN_POINT('Ctrl Pts',(0.00154289407701495,-0.004,0.00237844854507288));
#2737=CARTESIAN_POINT('Ctrl Pts',(0.00192713248193255,-0.004,0.00232683691852284));
#2738=CARTESIAN_POINT('Ctrl Pts',(0.00230938168164535,-0.004,0.00226249510068321));
#2739=CARTESIAN_POINT('',(0.0023094010767585,-0.004,0.00644273441009184));
#2740=CARTESIAN_POINT('',(0.00230940107675851,-0.004,0.0068));
#2741=CARTESIAN_POINT('',(0.,-0.004,0.0068));
#2742=CARTESIAN_POINT('Ctrl Pts',(-2.36670764249305E-18,-0.004,0.0068));
#2743=CARTESIAN_POINT('Ctrl Pts',(0.00107179676971335,-0.004,0.0068));
#2744=CARTESIAN_POINT('Ctrl Pts',(0.0023094010767308,-0.004,0.00644273441009984));
#2745=CARTESIAN_POINT('Ctrl Pts',(-0.00230940107682444,-0.004,0.0064427344100728));
#2746=CARTESIAN_POINT('Ctrl Pts',(-0.001071796769751,-0.004,0.0068));
#2747=CARTESIAN_POINT('Ctrl Pts',(-2.36670764249305E-18,-0.004,0.0068));
#2748=CARTESIAN_POINT('Origin',(0.00346410161513775,-0.002,0.0068));
#2749=CARTESIAN_POINT('',(0.00461879440075556,-3.31249001825354E-9,0.00226251801022538));
#2750=CARTESIAN_POINT('Ctrl Pts',(0.00230940691705295,-0.00399998988431329,
0.00226254053913407));
#2751=CARTESIAN_POINT('Ctrl Pts',(0.00250052112625622,-0.00366897036392487,
0.00232700363594613));
#2752=CARTESIAN_POINT('Ctrl Pts',(0.00269262130445346,-0.00333624309307501,
0.00237890074741045));
#2753=CARTESIAN_POINT('Ctrl Pts',(0.00288523530706997,-0.0030026258584546,
0.00241461216933168));
#2754=CARTESIAN_POINT('Ctrl Pts',(0.00307488976811388,-0.00267413470014111,
0.00244977488017086));
#2755=CARTESIAN_POINT('Ctrl Pts',(0.00326504319652788,-0.00234477935046048,
0.00246919460122286));
#2756=CARTESIAN_POINT('Ctrl Pts',(0.00345519948963801,-0.00201541895392154,
0.00246969208645215));
#2757=CARTESIAN_POINT('Ctrl Pts',(0.00345816686225689,-0.00201027931322678,
0.00246969984966642));
#2758=CARTESIAN_POINT('Ctrl Pts',(0.00346113423804048,-0.00200513966704103,
0.00246970300391282));
#2759=CARTESIAN_POINT('Ctrl Pts',(0.00346410161390816,-0.00200000002070232,
0.00246970156489885));
#2760=CARTESIAN_POINT('Ctrl Pts',(0.00365722549107684,-0.00166549961614694,
0.00246960791044806));
#2761=CARTESIAN_POINT('Ctrl Pts',(0.00385033581825397,-0.00133102273658185,
0.00244982678117351));
#2762=CARTESIAN_POINT('Ctrl Pts',(0.00404294431061012,-0.000997415041851751,
0.0024141390095264));
#2763=CARTESIAN_POINT('Ctrl Pts',(0.00423555280296627,-0.000663807347121655,
0.0023784512378793));
#2764=CARTESIAN_POINT('Ctrl Pts',(0.00442766851201849,-0.000331053178111084,
0.00232683813847981));
#2765=CARTESIAN_POINT('Ctrl Pts',(0.00461879248828856,-1.67406667481163E-8,
0.0022624954813167));
#2766=CARTESIAN_POINT('',(0.00461880215351701,0.,0.00644273441009184));
#2767=CARTESIAN_POINT('',(0.00461880215351701,0.,0.0068));
#2768=CARTESIAN_POINT('',(0.00346410161513775,-0.002,0.0068));
#2769=CARTESIAN_POINT('Ctrl Pts',(0.00461880215350315,-2.3987204103231E-14,
0.00644273441009984));
#2770=CARTESIAN_POINT('Ctrl Pts',(0.00399999999999443,-0.00107179676973414,
0.0068));
#2771=CARTESIAN_POINT('Ctrl Pts',(0.00346410161513775,-0.00200000000000001,
0.0068));
#2772=CARTESIAN_POINT('Ctrl Pts',(0.00346410161513775,-0.00200000000000001,
0.0068));
#2773=CARTESIAN_POINT('Ctrl Pts',(0.00292820323026226,-0.00292820323029846,
0.0068));
#2774=CARTESIAN_POINT('Ctrl Pts',(0.00230940107672555,-0.00400000000005708,
0.00644273441007281));
#2775=CARTESIAN_POINT('Origin',(0.00346410161513775,0.002,0.0068));
#2776=CARTESIAN_POINT('',(0.00230940003642643,0.00399999162966663,0.00226251781806703));
#2777=CARTESIAN_POINT('Ctrl Pts',(0.00461879631322256,1.01156867116092E-8,
0.00226254053913407));
#2778=CARTESIAN_POINT('Ctrl Pts',(0.00442768210401929,0.000331029636075126,
0.00232700363594612));
#2779=CARTESIAN_POINT('Ctrl Pts',(0.00423558192403006,0.000663756905890381,
0.00237890074741046));
#2780=CARTESIAN_POINT('Ctrl Pts',(0.00404296792501673,0.000997374142591087,
0.00241461216933168));
#2781=CARTESIAN_POINT('Ctrl Pts',(0.00385331346752063,0.0013258653029529,
0.00244977488017086));
#2782=CARTESIAN_POINT('Ctrl Pts',(0.0036631600820319,0.00165522067741644,
0.00246919460122286));
#2783=CARTESIAN_POINT('Ctrl Pts',(0.00347300375818372,0.00198458105620877,
0.00246969208645216));
#2784=CARTESIAN_POINT('Ctrl Pts',(0.00347003638508517,0.00198972069662659,
0.00246969984966643));
#2785=CARTESIAN_POINT('Ctrl Pts',(0.00346706900881365,0.00199486034253063,
0.00246970300391284));
#2786=CARTESIAN_POINT('Ctrl Pts',(0.0034641016324517,0.00199999998858397,
0.00246970156489887));
#2787=CARTESIAN_POINT('Ctrl Pts',(0.00327097772311491,0.00233450037456708,
0.00246960791044809));
#2788=CARTESIAN_POINT('Ctrl Pts',(0.00307786741202155,0.00266897726341816,
0.00244982678117361));
#2789=CARTESIAN_POINT('Ctrl Pts',(0.00288525891966539,0.00300258495814827,
0.00241413900952655));
#2790=CARTESIAN_POINT('Ctrl Pts',(0.00269265042730923,0.00333619265287837,
0.00237845123787949));
#2791=CARTESIAN_POINT('Ctrl Pts',(0.002500534718257,0.00366894682188895,
0.00232683813848));
#2792=CARTESIAN_POINT('Ctrl Pts',(0.00230941074198695,0.00399998325933327,
0.00226249548131679));
#2793=CARTESIAN_POINT('',(0.00230940107675851,0.004,0.00644273441009184));
#2794=CARTESIAN_POINT('',(0.00230940107675851,0.004,0.0068));
#2795=CARTESIAN_POINT('',(0.00346410161513775,0.002,0.0068));
#2796=CARTESIAN_POINT('Ctrl Pts',(0.00230940107677235,0.003999999999976,
0.00644273441009984));
#2797=CARTESIAN_POINT('Ctrl Pts',(0.00292820323028107,0.00292820323026587,
0.0068));
#2798=CARTESIAN_POINT('Ctrl Pts',(0.00346410161513774,0.00200000000000001,
0.0068));
#2799=CARTESIAN_POINT('Ctrl Pts',(0.00346410161513774,0.00200000000000001,
0.0068));
#2800=CARTESIAN_POINT('Ctrl Pts',(0.00400000000001324,0.00107179676970155,
0.00680000000000001));
#2801=CARTESIAN_POINT('Ctrl Pts',(0.00461880215354997,-5.70991966576601E-14,
0.00644273441007281));
#2802=CARTESIAN_POINT('Origin',(0.,0.004,0.0068));
#2803=CARTESIAN_POINT('Ctrl Pts',(0.00230938933086591,0.004,0.00226254015481727));
#2804=CARTESIAN_POINT('Ctrl Pts',(0.00192715966343552,0.004,0.00232700240167072));
#2805=CARTESIAN_POINT('Ctrl Pts',(0.00154295236666105,0.00399999999907498,
0.00237889805720109));
#2806=CARTESIAN_POINT('Ctrl Pts',(0.00115771798562292,0.00400000000093493,
0.00241461091731328));
#2807=CARTESIAN_POINT('Ctrl Pts',(0.00077837318028794,0.00400000000276645,
0.00244977778879215));
#2808=CARTESIAN_POINT('Ctrl Pts',(0.000398030391648709,0.00400000002730032,
0.00246919770092989));
#2809=CARTESIAN_POINT('Ctrl Pts',(1.76878773571683E-5,0.00400000000992256,
0.00246969318518198));
#2810=CARTESIAN_POINT('Ctrl Pts',(1.1782811571249E-5,0.00400000000965276,
0.0024697008778984));
#2811=CARTESIAN_POINT('Ctrl Pts',(5.87774094490613E-6,0.00400000000937819,
0.00246970400775273));
#2812=CARTESIAN_POINT('Ctrl Pts',(-2.73285226471042E-8,0.00400000000909995,
0.00246970259022018));
#2813=CARTESIAN_POINT('Ctrl Pts',(-0.000386275149414076,0.00399999999090037,
0.00246960987008162));
#2814=CARTESIAN_POINT('Ctrl Pts',(-0.000772489689067513,0.004,0.00244982989983513));
#2815=CARTESIAN_POINT('Ctrl Pts',(-0.00115770017497109,0.004,0.00241414191963193));
#2816=CARTESIAN_POINT('Ctrl Pts',(-0.00154291066087466,0.004,0.00237845393942873));
#2817=CARTESIAN_POINT('Ctrl Pts',(-0.00192713509457193,0.004,0.00232683936300356));
#2818=CARTESIAN_POINT('Ctrl Pts',(-0.00230938181107929,0.004,0.00226249586266454));
#2819=CARTESIAN_POINT('',(0.,0.004,0.0068));
#2820=CARTESIAN_POINT('Ctrl Pts',(-0.00230940107673081,0.004,0.00644273441009983));
#2821=CARTESIAN_POINT('Ctrl Pts',(-0.00107179676971336,0.004,0.0068));
#2822=CARTESIAN_POINT('Ctrl Pts',(1.18335392355646E-17,0.004,0.0068));
#2823=CARTESIAN_POINT('Ctrl Pts',(1.18335392355646E-17,0.004,0.0068));
#2824=CARTESIAN_POINT('Ctrl Pts',(0.001071796769751,0.004,0.0068));
#2825=CARTESIAN_POINT('Ctrl Pts',(0.00230940107682445,0.004,0.0064427344100728));
#2826=CARTESIAN_POINT('Origin',(0.,0.,0.0068));
#2827=CARTESIAN_POINT('Origin',(0.,0.,0.0068));
#2828=CARTESIAN_POINT('Origin',(0.,0.,0.0068));
#2829=CARTESIAN_POINT('Origin',(0.,0.,0.0068));
#2830=CARTESIAN_POINT('Origin',(0.,0.,0.0068));
#2831=CARTESIAN_POINT('Origin',(0.,0.,0.0068));
#2832=CARTESIAN_POINT('Origin',(0.,0.,0.0068));
#2833=CARTESIAN_POINT('Origin',(0.,0.,0.0068));
#2834=CARTESIAN_POINT('Origin',(0.,0.,0.0068));
#2835=CARTESIAN_POINT('Origin',(0.,0.,0.0068));
#2836=CARTESIAN_POINT('Origin',(0.,0.,0.0068));
#2837=CARTESIAN_POINT('Origin',(0.,0.,0.0068));
#2838=CARTESIAN_POINT('Origin',(-8.67361737988404E-19,-8.67361737988404E-19,
0.0068));
#2839=CARTESIAN_POINT('Origin',(0.,0.,0.000567100162269167));
#2840=CARTESIAN_POINT('',(0.00699395967877932,0.,0.0011));
#2841=CARTESIAN_POINT('',(-0.00699395967877932,-8.56513033398275E-19,0.0011));
#2842=CARTESIAN_POINT('Origin',(0.,0.,0.0011));
#2843=CARTESIAN_POINT('Origin',(0.,0.,0.0011));
#2844=CARTESIAN_POINT('',(-0.0068,-8.327598234202E-19,0.));
#2845=CARTESIAN_POINT('Origin',(-0.0068,-8.327598234202E-19,0.000567100162269167));
#2846=CARTESIAN_POINT('Origin',(0.,0.,0.));
#2847=CARTESIAN_POINT('Origin',(0.,0.,-0.36032464112347));
#2848=CARTESIAN_POINT('',(0.00494387431153844,1.1921208113455E-18,0.00184617005138037));
#2849=CARTESIAN_POINT('',(1.,-1.22464679914735E-16,-0.36032464112347));
#2850=CARTESIAN_POINT('',(0.00247193941718072,-0.00428151672012047,0.00184617090911052));
#2851=CARTESIAN_POINT('Ctrl Pts',(0.00494387431153844,1.1921208113455E-18,
0.00184617005138037));
#2852=CARTESIAN_POINT('Ctrl Pts',(0.00452747332878781,-0.000701807087018258,
0.0019977276146208));
#2853=CARTESIAN_POINT('Ctrl Pts',(0.00368750878396646,-0.00212220560039757,
0.0021900207622692));
#2854=CARTESIAN_POINT('Ctrl Pts',(0.00287197920564823,-0.00356918468363283,
0.00199790178196429));
#2855=CARTESIAN_POINT('Ctrl Pts',(0.00247193941718072,-0.00428151672012047,
0.00184617090911052));
#2856=CARTESIAN_POINT('',(-0.002471932361137,-0.00428152068985298,0.00184617094191608));
#2857=CARTESIAN_POINT('Ctrl Pts',(0.00247193715576922,-0.00428152074690959,
0.00184617005138037));
#2858=CARTESIAN_POINT('Ctrl Pts',(0.00165595444467786,-0.00427181046769567,
0.00199772751317215));
#2859=CARTESIAN_POINT('Ctrl Pts',(5.82745458661851E-6,-0.00425457905249832,
0.00219002124928115));
#2860=CARTESIAN_POINT('Ctrl Pts',(-0.00165501952187246,-0.00427179934699393,
0.00199790093446101));
#2861=CARTESIAN_POINT('Ctrl Pts',(-0.002471932361137,-0.00428152068985298,
0.00184617094191608));
#2862=CARTESIAN_POINT('',(-0.00494387188482622,-4.09000919964499E-9,0.00184617093463073));
#2863=CARTESIAN_POINT('Ctrl Pts',(-0.00247193715576922,-0.00428152074690959,
0.00184617005138037));
#2864=CARTESIAN_POINT('Ctrl Pts',(-0.00287151943030767,-0.00357000337417761,
0.0019977276146208));
#2865=CARTESIAN_POINT('Ctrl Pts',(-0.00368163833127164,-0.00213237352369449,
0.00219002075687879));
#2866=CARTESIAN_POINT('Ctrl Pts',(-0.00452699416225394,-0.000702614689574446,
0.00199790179273536));
#2867=CARTESIAN_POINT('Ctrl Pts',(-0.00494387188482622,-4.09000919964499E-9,
0.00184617093463073));
#2868=CARTESIAN_POINT('',(-0.00247193937985183,0.00428151678659028,0.00184617089495207));
#2869=CARTESIAN_POINT('Ctrl Pts',(-0.00494387431153844,-1.74540774594479E-18,
0.00184617005138037));
#2870=CARTESIAN_POINT('Ctrl Pts',(-0.0045274733287878,0.000701807087018257,
0.0019977276146208));
#2871=CARTESIAN_POINT('Ctrl Pts',(-0.00368750877090321,0.00212220562248781,
0.00219002076525978));
#2872=CARTESIAN_POINT('Ctrl Pts',(-0.00287197918028176,0.00356918472864007,
0.00199790177598857));
#2873=CARTESIAN_POINT('Ctrl Pts',(-0.00247193937985182,0.00428151678659028,
0.00184617089495207));
#2874=CARTESIAN_POINT('',(0.0024719326136737,0.0042815206928582,0.00184617089501096));
#2875=CARTESIAN_POINT('Ctrl Pts',(-0.00247193715576922,0.00428152074690959,
0.00184617005138037));
#2876=CARTESIAN_POINT('Ctrl Pts',(-0.00165595333332649,0.00427181045447048,
0.00199772771959024));
#2877=CARTESIAN_POINT('Ctrl Pts',(-5.91333274921904E-6,0.00425457911567813,
0.00219002026760492));
#2878=CARTESIAN_POINT('Ctrl Pts',(0.00165501039761641,0.00427179923815414,
0.00199790264112614));
#2879=CARTESIAN_POINT('Ctrl Pts',(0.0024719326136737,0.0042815206928582,
0.00184617089501096));
#2880=CARTESIAN_POINT('Ctrl Pts',(0.00247193715576921,0.00428152074690959,
0.00184617005138037));
#2881=CARTESIAN_POINT('Ctrl Pts',(0.00287151943030767,0.0035700033741776,
0.0019977276146208));
#2882=CARTESIAN_POINT('Ctrl Pts',(0.00368163838375097,0.00213237343056514,
0.0021900207693355));
#2883=CARTESIAN_POINT('Ctrl Pts',(0.00452699427177788,0.000702614504335504,
0.00199790176784451));
#2884=CARTESIAN_POINT('Ctrl Pts',(0.00494387204685787,3.81691914936205E-9,
0.00184617087565612));
#2885=CARTESIAN_POINT('Origin',(-8.67361737988404E-19,-8.67361737988404E-19,
0.));
#2886=CARTESIAN_POINT('',(-0.00325,-3.9801020972289E-19,0.));
#2887=CARTESIAN_POINT('Origin',(0.,0.,0.));
#2888=CARTESIAN_POINT('Ctrl Pts',(0.0020802062398655,-0.00439697710233114,
0.00217924420147432));
#2889=CARTESIAN_POINT('Ctrl Pts',(0.00210856163081419,-0.00434786412453955,
0.00188755760062778));
#2890=CARTESIAN_POINT('Ctrl Pts',(0.00236295304044323,-0.00447615069376761,
0.00180329134165063));
#2891=CARTESIAN_POINT('Ctrl Pts',(0.00252613349767768,-0.00362460843532059,
0.00235256917709083));
#2892=CARTESIAN_POINT('Ctrl Pts',(0.002542066495585,-0.00359701167342807,
0.00206498114514791));
#2893=CARTESIAN_POINT('Ctrl Pts',(0.00279156587787958,-0.00371262340768279,
0.00197661181143248));
#2894=CARTESIAN_POINT('Ctrl Pts',(0.00345081170624761,-0.0020230187974257,
0.00258494001506871));
#2895=CARTESIAN_POINT('Ctrl Pts',(0.00345100992757241,-0.00202267546802013,
0.0023096133598543));
#2896=CARTESIAN_POINT('Ctrl Pts',(0.00367050135085753,-0.00214874606333825,
0.0022089697386081));
#2897=CARTESIAN_POINT('Ctrl Pts',(0.00439304074880029,-0.000391030223357476,
0.00235667923254302));
#2898=CARTESIAN_POINT('Ctrl Pts',(0.0043774784205849,-0.000417984966510446,
0.00206916499501039));
#2899=CARTESIAN_POINT('Ctrl Pts',(0.00460190032261363,-0.000576511435992028,
0.00198072177999877));
#2900=CARTESIAN_POINT('Ctrl Pts',(0.00485097725303226,0.000402139068612779,
0.00217804861127444));
#2901=CARTESIAN_POINT('Ctrl Pts',(0.00482257756304232,0.00035294936263097,
0.00188631450420623));
#2902=CARTESIAN_POINT('Ctrl Pts',(0.00506092745585843,0.000196726460696005,
0.00180209579967309));
#2903=CARTESIAN_POINT('Ctrl Pts',(0.00461880215502372,2.60969660665088E-12,
0.00226249222696017));
#2904=CARTESIAN_POINT('Ctrl Pts',(0.00461880493041573,4.80972967263351E-9,
0.00221981071831767));
#2905=CARTESIAN_POINT('Ctrl Pts',(0.00462646565353065,9.25513802947402E-9,
0.00217761263137423));
#2906=CARTESIAN_POINT('Ctrl Pts',(0.00465632814594096,1.66558839052706E-8,
0.00209286153099971));
#2907=CARTESIAN_POINT('Ctrl Pts',(0.00467967919928059,1.93291946404923E-8,
0.00205143483680694));
#2908=CARTESIAN_POINT('Ctrl Pts',(0.00473623848218349,2.17963502552309E-8,
0.00197900347582149));
#2909=CARTESIAN_POINT('Ctrl Pts',(0.00476871684204161,2.16941492436947E-8,
0.00194773373134783));
#2910=CARTESIAN_POINT('Ctrl Pts',(0.00484002106628586,1.99446438725073E-8,
0.00189466116743958));
#2911=CARTESIAN_POINT('Ctrl Pts',(0.00487876012895213,7.20229918431176E-9,
0.00187273694245961));
#2912=CARTESIAN_POINT('Ctrl Pts',(0.00492753919099201,2.65052329180053E-8,
0.00185233276034135));
#2913=CARTESIAN_POINT('Ctrl Pts',(0.0049356821302962,1.06563597029485E-8,
0.00184914982572676));
#2914=CARTESIAN_POINT('Ctrl Pts',(0.00494387279830003,9.92076541137559E-9,
0.00184616902333901));
#2915=CARTESIAN_POINT('Ctrl Pts',(0.00230940107982304,-0.004,0.00226249183548786));
#2916=CARTESIAN_POINT('Ctrl Pts',(0.00230940667748031,-0.00400000000000001,
0.00221981045876485));
#2917=CARTESIAN_POINT('Ctrl Pts',(0.0023132409100976,-0.0040066321208989,
0.00217761250549695));
#2918=CARTESIAN_POINT('Ctrl Pts',(0.00232817856401501,-0.00403248997215914,
0.00209286164541814));
#2919=CARTESIAN_POINT('Ctrl Pts',(0.00233985638039947,-0.00405271115271212,
0.00205143505643002));
#2920=CARTESIAN_POINT('Ctrl Pts',(0.00236813813045257,-0.00410169160548647,
0.0019790036952096));
#2921=CARTESIAN_POINT('Ctrl Pts',(0.0023843772427971,-0.00412981877908601,
0.00194773388444953));
#2922=CARTESIAN_POINT('Ctrl Pts',(0.00242002790301579,-0.00419157106220532,
0.00189466118804628));
#2923=CARTESIAN_POINT('Ctrl Pts',(0.00243938639823226,-0.00422512665324962,
0.00187273688517089));
#2924=CARTESIAN_POINT('Ctrl Pts',(0.00246379267336123,-0.00426736064254826,
0.00185233281178718));
#2925=CARTESIAN_POINT('Ctrl Pts',(0.00246785033449192,-0.00427442067365005,
0.00184914985094565));
#2926=CARTESIAN_POINT('Ctrl Pts',(0.00247194491204864,-0.00428151417461562,
0.00184616912670582));
#2927=CARTESIAN_POINT('Ctrl Pts',(-0.00276909135727935,-0.004,0.00217899169790385));
#2928=CARTESIAN_POINT('Ctrl Pts',(-0.00271235704649767,-0.00399999999999999,
0.00188729521822938));
#2929=CARTESIAN_POINT('Ctrl Pts',(-0.00269626039969526,-0.00428446969999985,
0.00180303837461786));
#2930=CARTESIAN_POINT('Ctrl Pts',(-0.00187685966992971,-0.004,0.00235244886375929));
#2931=CARTESIAN_POINT('Ctrl Pts',(-0.00184499447367401,-0.00400000000000006,
0.00206485113824212));
#2932=CARTESIAN_POINT('Ctrl Pts',(-0.00182033920767984,-0.00427389079720739,
0.00197649100614117));
#2933=CARTESIAN_POINT('Ctrl Pts',(-2.68059993290473E-5,-0.004,0.00258505308205348));
#2934=CARTESIAN_POINT('Ctrl Pts',(-2.64037614343951E-5,-0.00399999999999977,
0.00230972896816672));
#2935=CARTESIAN_POINT('Ctrl Pts',(-2.58366266104264E-5,-0.00425311179830988,
0.00220908222014014));
#2936=CARTESIAN_POINT('Ctrl Pts',(0.00185878890297778,-0.004,0.00235657272456735));
#2937=CARTESIAN_POINT('Ctrl Pts',(0.00182766695568966,-0.00400000000000039,
0.00206904911217261));
#2938=CARTESIAN_POINT('Ctrl Pts',(0.00180255912815774,-0.00427362955430766,
0.00198061477916247));
#2939=CARTESIAN_POINT('Ctrl Pts',(0.00277510174796861,-0.004,0.00217778485182945));
#2940=CARTESIAN_POINT('Ctrl Pts',(0.00271827814865782,-0.00399999999999991,
0.00188604038028264));
#2941=CARTESIAN_POINT('Ctrl Pts',(0.00270215958680058,-0.00428454621889335,
0.00180183157755754));
#2942=CARTESIAN_POINT('Ctrl Pts',(-0.00230940107522602,-0.00400000000265434,
0.00226249222695167));
#2943=CARTESIAN_POINT('Ctrl Pts',(-0.00230939827617001,-0.00400000485076157,
0.0022198103539442));
#2944=CARTESIAN_POINT('Ctrl Pts',(-0.00231322483018635,-0.00400664160220837,
0.00217761191602451));
#2945=CARTESIAN_POINT('Ctrl Pts',(-0.00232814975025645,-0.00403250724714706,
0.00209286083905841));
#2946=CARTESIAN_POINT('Ctrl Pts',(-0.00233982289833555,-0.00405273112360759,
0.00205143444336701));
#2947=CARTESIAN_POINT('Ctrl Pts',(-0.00236810006107592,-0.0041017135810827,
0.00197900396916589));
#2948=CARTESIAN_POINT('Ctrl Pts',(-0.00238433899975335,-0.00412984004164373,
0.00194773472029215));
#2949=CARTESIAN_POINT('Ctrl Pts',(-0.0024199904598784,-0.00419158665219816,
0.00189466492377884));
#2950=CARTESIAN_POINT('Ctrl Pts',(-0.00243936900505325,-0.00422512562446801,
0.00187274224654465));
#2951=CARTESIAN_POINT('Ctrl Pts',(-0.00246374483466011,-0.00426738465712574,
0.00185233386579348));
#2952=CARTESIAN_POINT('Ctrl Pts',(-0.00246782572589702,-0.00427442103508152,
0.00184915496726748));
#2953=CARTESIAN_POINT('Ctrl Pts',(-0.00247192721594409,-0.00428152353602606,
0.00184617013594552));
#2954=CARTESIAN_POINT('Ctrl Pts',(0.00484799699036367,-0.000396977102250874,
0.00217924420149234));
#2955=CARTESIAN_POINT('Ctrl Pts',(0.0048196415994154,-0.000347864124460288,
0.00188755760064398));
#2956=CARTESIAN_POINT('Ctrl Pts',(0.00505793673214804,-0.000191697985830489,
0.00180329134166766));
#2957=CARTESIAN_POINT('Ctrl Pts',(0.00440206973256443,0.000375391564737258,
0.00235256917709936));
#2958=CARTESIAN_POINT('Ctrl Pts',(0.00438613673465794,0.00040298832662938,
0.00206498114515469));
#2959=CARTESIAN_POINT('Ctrl Pts',(0.00461100912464618,0.000561255262797908,
0.00197661181144046));
#2960=CARTESIAN_POINT('Ctrl Pts',(0.0034773915240279,0.00197698120257433,
0.00258494001506013));
#2961=CARTESIAN_POINT('Ctrl Pts',(0.00347719330270246,0.00197732453198037,
0.0023096133598436));
#2962=CARTESIAN_POINT('Ctrl Pts',(0.00369611935256539,0.00210437438280086,
0.00220896973859817));
#2963=CARTESIAN_POINT('Ctrl Pts',(0.00253516248150867,0.00360896977658459,
0.00235667923255163));
#2964=CARTESIAN_POINT('Ctrl Pts',(0.00255072480972449,0.00358201503343101,
0.00206916499501691));
#2965=CARTESIAN_POINT('Ctrl Pts',(0.00280022371048194,0.00369710686701457,
0.00198072178000659));
#2966=CARTESIAN_POINT('Ctrl Pts',(0.002077225977291,0.00440213906853008,
0.00217804861129297));
#2967=CARTESIAN_POINT('Ctrl Pts',(0.00210562566728017,0.00435294936254953,
0.00188631450422304));
#2968=CARTESIAN_POINT('Ctrl Pts',(0.00236009361541863,0.00448125497375149,
0.00180209579969069));
#2969=CARTESIAN_POINT('Ctrl Pts',(0.0023094010752774,0.00400000000256537,
0.00226249222696888));
#2970=CARTESIAN_POINT('Ctrl Pts',(0.0023093983235636,0.00400000476867347,
0.00221981080901497));
#2971=CARTESIAN_POINT('Ctrl Pts',(0.00231322484200826,0.0040066413091479,
0.00217761280825381));
#2972=CARTESIAN_POINT('Ctrl Pts',(0.00232814966084154,0.00403250653132782,
0.00209286186351978));
#2973=CARTESIAN_POINT('Ctrl Pts',(0.0023398228431364,0.00405273037837203,
0.00205143523833409));
#2974=CARTESIAN_POINT('Ctrl Pts',(0.00236810032719515,0.0041017133110918,
0.00197900379862345));
#2975=CARTESIAN_POINT('Ctrl Pts',(0.00238433962881604,0.00412984040412892,
0.00194773394920763));
#2976=CARTESIAN_POINT('Ctrl Pts',(0.00241999332152723,0.00419159094343347,
0.00189466123632128));
#2977=CARTESIAN_POINT('Ctrl Pts',(0.00243937381272943,0.00422513365863828,
0.00187273698229547));
#2978=CARTESIAN_POINT('Ctrl Pts',(0.00246374684853763,0.00426738730103737,
0.00185233273837006));
#2979=CARTESIAN_POINT('Ctrl Pts',(0.00246783178595212,0.00427443117503508,
0.00184914992183635));
#2980=CARTESIAN_POINT('Ctrl Pts',(0.00247192773993968,0.00428152411588965,
0.00184616912415846));
#2981=CARTESIAN_POINT('Ctrl Pts',(-0.00484799699031254,0.000396977102162332,
0.00217924420151239));
#2982=CARTESIAN_POINT('Ctrl Pts',(-0.00481964159936525,0.000347864124373369,
0.00188755760066478));
#2983=CARTESIAN_POINT('Ctrl Pts',(-0.00505793673209653,0.000191697985744254,
0.00180329134168764));
#2984=CARTESIAN_POINT('Ctrl Pts',(-0.00440206973252995,-0.000375391564796995,
0.00235256917710718));
#2985=CARTESIAN_POINT('Ctrl Pts',(-0.00438613673462329,-0.000402988326689221,
0.00206498114516339));
#2986=CARTESIAN_POINT('Ctrl Pts',(-0.00461100912461266,-0.000561255262855402,
0.0019766118114488));
#2987=CARTESIAN_POINT('Ctrl Pts',(-0.00347739152402765,-0.00197698120257474,
0.0025849400150519));
#2988=CARTESIAN_POINT('Ctrl Pts',(-0.00347719330270223,-0.00197732453198073,
0.00230961335983513));
#2989=CARTESIAN_POINT('Ctrl Pts',(-0.00369611935256536,-0.00210437438280157,
0.0022089697385899));
#2990=CARTESIAN_POINT('Ctrl Pts',(-0.00253516248154363,-0.00360896977652404,
0.00235667923256029));
#2991=CARTESIAN_POINT('Ctrl Pts',(-0.00255072480975946,-0.00358201503337074,
0.00206916499502631));
#2992=CARTESIAN_POINT('Ctrl Pts',(-0.00280022371051508,-0.00369710686695539,
0.00198072178001496));
#2993=CARTESIAN_POINT('Ctrl Pts',(-0.00207722597734354,-0.00440213906843907,
0.00217804861131337));
#2994=CARTESIAN_POINT('Ctrl Pts',(-0.0021056256673318,-0.00435294936246005,
0.00188631450424426));
#2995=CARTESIAN_POINT('Ctrl Pts',(-0.00236009361546901,-0.00448125497366147,
0.00180209579971121));
#2996=CARTESIAN_POINT('Ctrl Pts',(-0.00461880215502371,-2.60969740465829E-12,
0.00226249222696032));
#2997=CARTESIAN_POINT('Ctrl Pts',(-0.00461880493044008,-4.80977186674728E-9,
0.00221981034336869));
#2998=CARTESIAN_POINT('Ctrl Pts',(-0.00462646578784855,-9.25521530506121E-9,
0.00217761189364838));
#2999=CARTESIAN_POINT('Ctrl Pts',(-0.00465632853642066,-1.66559319787286E-8,
0.00209286081607735));
#3000=CARTESIAN_POINT('Ctrl Pts',(-0.00467967949048832,-1.93292113464515E-8,
0.00205143443431073));
#3001=CARTESIAN_POINT('Ctrl Pts',(-0.00473623815244463,-2.17963318402135E-8,
0.00197900392609519));
#3002=CARTESIAN_POINT('Ctrl Pts',(-0.00476871590488861,-2.16941546676782E-8,
0.0019477346444674));
#3003=CARTESIAN_POINT('Ctrl Pts',(-0.00484001587792066,-1.99447883239839E-8,
0.00189466481646245));
#3004=CARTESIAN_POINT('Ctrl Pts',(-0.0048787507470625,-7.2202173171277E-9,
0.00187274215724451));
#3005=CARTESIAN_POINT('Ctrl Pts',(-0.00492753617461704,-2.64997623468435E-8,
0.00185233376728398));
#3006=CARTESIAN_POINT('Ctrl Pts',(-0.00493567013491418,-1.06587769589897E-8,
0.0018491549351575));
#3007=CARTESIAN_POINT('Ctrl Pts',(-0.00494387177388727,-9.92086063382213E-9,
0.00184617012407515));
#3008=CARTESIAN_POINT('Ctrl Pts',(0.00276648183574491,0.004,0.00217949823698557));
#3009=CARTESIAN_POINT('Ctrl Pts',(0.00270979471839317,0.00399999999999989,
0.00188782157682243));
#3010=CARTESIAN_POINT('Ctrl Pts',(0.00269369884333924,0.00428443560947813,
0.00180354584308321));
#3011=CARTESIAN_POINT('Ctrl Pts',(0.00187500692923374,0.004,0.00235269014572225));
#3012=CARTESIAN_POINT('Ctrl Pts',(0.00184314015037907,0.00400000000000045,
0.00206511185901196));
#3013=CARTESIAN_POINT('Ctrl Pts',(0.00181854159277439,0.0042738664773099,
0.00197673327463295));
#3014=CARTESIAN_POINT('Ctrl Pts',(2.63535568577022E-5,0.004,0.00258482628539704));
#3015=CARTESIAN_POINT('Ctrl Pts',(2.59629106265878E-5,0.00399999999999955,
0.00230949707126385));
#3016=CARTESIAN_POINT('Ctrl Pts',(2.53992995043738E-5,0.00425312914551421,
0.00220885659731835));
#3017=CARTESIAN_POINT('Ctrl Pts',(-0.00185696196096345,0.004,0.00235678640664226));
#3018=CARTESIAN_POINT('Ctrl Pts',(-0.00182583461132829,0.0040000000000005,
0.00206928159589147));
#3019=CARTESIAN_POINT('Ctrl Pts',(-0.00180078859598649,0.00427360698479904,
0.00198082944956426));
#3020=CARTESIAN_POINT('Ctrl Pts',(-0.00277239243853729,0.004,0.00217831389249534));
#3021=CARTESIAN_POINT('Ctrl Pts',(-0.00271561741455655,0.00399999999999988,
0.00188659021085909));
#3022=CARTESIAN_POINT('Ctrl Pts',(-0.00269949989932968,0.00428451070179002,
0.00180236154602939));
#3023=CARTESIAN_POINT('Ctrl Pts',(-0.00230940107972112,0.004,0.00226249261916749));
#3024=CARTESIAN_POINT('Ctrl Pts',(-0.00230940658357872,0.00400000000000002,
0.00221981070558142));
#3025=CARTESIAN_POINT('Ctrl Pts',(-0.00231324082258085,0.00400663228001755,
0.0021776122207903));
#3026=CARTESIAN_POINT('Ctrl Pts',(-0.00232817854337327,0.0040324904929674,
0.00209286106268009));
#3027=CARTESIAN_POINT('Ctrl Pts',(-0.00233985631668495,0.00405271168730321,
0.00205143463328512));
#3028=CARTESIAN_POINT('Ctrl Pts',(-0.00236813776484925,0.00410169169915766,
0.00197900406377293));
#3029=CARTESIAN_POINT('Ctrl Pts',(-0.00238437654793324,0.00412981829929945,
0.00194773476157516));
#3030=CARTESIAN_POINT('Ctrl Pts',(-0.00242002502086811,0.00419156673501641,
0.00189466489996567));
#3031=CARTESIAN_POINT('Ctrl Pts',(-0.00243938148784039,0.00422511835941925,
0.00187274224703594));
#3032=CARTESIAN_POINT('Ctrl Pts',(-0.00246379100631313,0.00426735863971814,
0.00185233363819034));
#3033=CARTESIAN_POINT('Ctrl Pts',(-0.00246784451355287,0.00427441094564068,
0.00184915470496365));
#3034=CARTESIAN_POINT('Ctrl Pts',(-0.00247194489770891,0.00428151448007287,
0.00184616976692702));
#3035=CARTESIAN_POINT('Ctrl Pts',(-0.00208020623988541,0.00439697710229665,
0.00217924420148206));
#3036=CARTESIAN_POINT('Ctrl Pts',(-0.00210856163083422,0.00434786412450488,
0.00188755760063093));
#3037=CARTESIAN_POINT('Ctrl Pts',(-0.00236295304046781,0.00447615069373628,
0.00180329134165656));
#3038=CARTESIAN_POINT('Ctrl Pts',(-0.00252613349769144,0.00362460843529674,
0.0023525691770943));
#3039=CARTESIAN_POINT('Ctrl Pts',(-0.00254206649559906,0.00359701167340373,
0.0020649811451469));
#3040=CARTESIAN_POINT('Ctrl Pts',(-0.00279156587789806,0.00371262340766202,
0.00197661181143402));
#3041=CARTESIAN_POINT('Ctrl Pts',(-0.00345081170624774,0.00202301879742548,
0.00258494001506496));
#3042=CARTESIAN_POINT('Ctrl Pts',(-0.00345100992757254,0.00202267546801992,
0.00230961335984592));
#3043=CARTESIAN_POINT('Ctrl Pts',(-0.00367050135086289,0.00214874606334101,
0.00220896973860242));
#3044=CARTESIAN_POINT('Ctrl Pts',(-0.00439304074878628,0.000391030223381733,
0.00235667923254706));
#3045=CARTESIAN_POINT('Ctrl Pts',(-0.00437747842057059,0.000417984966535182,
0.00206916499501008));
#3046=CARTESIAN_POINT('Ctrl Pts',(-0.00460190032260445,0.000576511436018824,
0.00198072178000032));
#3047=CARTESIAN_POINT('Ctrl Pts',(-0.0048509772530118,-0.000402139068577363,
0.00217804861128226));
#3048=CARTESIAN_POINT('Ctrl Pts',(-0.00482257756302177,-0.000352949362595358,
0.00188631450420942));
#3049=CARTESIAN_POINT('Ctrl Pts',(-0.0050609274558431,-0.000196726460658123,
0.00180209579967924));
#3050=CARTESIAN_POINT('Origin',(0.,0.,-0.025));
#3051=CARTESIAN_POINT('',(-0.003,-3.67394039744206E-19,-0.000249999999999999));
#3052=CARTESIAN_POINT('Origin',(0.,0.,-0.00025));
#3053=CARTESIAN_POINT('',(-0.003,0.,-0.024458734125));
#3054=CARTESIAN_POINT('',(-0.003,-3.67394039744206E-19,-0.025));
#3055=CARTESIAN_POINT('Origin',(0.,0.,-0.024458734125));
#3056=CARTESIAN_POINT('Origin',(0.,0.,-0.025));
#3057=CARTESIAN_POINT('',(-0.002458734125,0.,-0.025));
#3058=CARTESIAN_POINT('Origin',(0.,0.,-0.025));
#3059=CARTESIAN_POINT('Origin',(0.,0.,-0.00025));
#3060=CARTESIAN_POINT('Origin',(-0.00325,-3.9801020972289E-19,-0.00025));
#3061=CARTESIAN_POINT('Origin',(0.,0.,-0.025));
#3062=CARTESIAN_POINT('',(-0.002458734125,-3.01108087613562E-19,-0.025));
#3821=UNCERTAINTY_MEASURE_WITH_UNIT(LENGTH_MEASURE(1.E-5),#3833,
'DISTANCE_ACCURACY_VALUE',
'Maximum model space distance between geometric entities at asserted c
onnectivities');
#3824=UNCERTAINTY_MEASURE_WITH_UNIT(LENGTH_MEASURE(1.E-5),#3833,
'DISTANCE_ACCURACY_VALUE',
'Maximum model space distance between geometric entities at asserted c
onnectivities');
#3829=(
GEOMETRIC_REPRESENTATION_CONTEXT(3)
GLOBAL_UNCERTAINTY_ASSIGNED_CONTEXT((#3821))
GLOBAL_UNIT_ASSIGNED_CONTEXT((#3833,#3834,#3835))
REPRESENTATION_CONTEXT('','3D')
);
#3832=(
GEOMETRIC_REPRESENTATION_CONTEXT(3)
GLOBAL_UNCERTAINTY_ASSIGNED_CONTEXT((#3824))
GLOBAL_UNIT_ASSIGNED_CONTEXT((#3833,#3834,#3835))
REPRESENTATION_CONTEXT('','3D')
);
#3833=(
LENGTH_UNIT()
NAMED_UNIT(*)
SI_UNIT($,.METRE.)
);
#3834=(
NAMED_UNIT(*)
PLANE_ANGLE_UNIT()
SI_UNIT($,.RADIAN.)
);
#3835=(
NAMED_UNIT(*)
SI_UNIT($,.STERADIAN.)
SOLID_ANGLE_UNIT()
);
#3840=SHAPE_DEFINITION_REPRESENTATION(#3847,#3866);
#3847=PRODUCT_DEFINITION_SHAPE('',$,#3874);
#3866=SHAPE_REPRESENTATION('',(#1915),#3829);
#3869=PRODUCT_DEFINITION_CONTEXT('part definition',#3892,'design');
#3874=PRODUCT_DEFINITION('2026-10-07-15-36-29-757',
'Hex flange bolt small M6x1.00 x 25',#3881,#3869);
#3881=PRODUCT_DEFINITION_FORMATION('',$,#3898);
#3892=APPLICATION_CONTEXT(
'Core Data for Automotive Mechanical Design Process');
#3893=PRODUCT_CONTEXT('part definition',#3892,'mechanical');
#3898=PRODUCT('2026-10-07-15-36-29-757',
'Hex flange bolt small M6x1.00 x 25',
'Hex flange bolt small M6x1.00 x 25',(#3893));
#3905=PRESENTATION_STYLE_ASSIGNMENT((#3911));
#3911=SURFACE_STYLE_USAGE(.BOTH.,#3917);
#3917=SURFACE_SIDE_STYLE('',(#3923));
#3923=SURFACE_STYLE_FILL_AREA(#3929);
#3929=FILL_AREA_STYLE('Opaque(154,165,175)',(#3935));
#3935=FILL_AREA_STYLE_COLOUR('Opaque(154,165,175)',#3941);
#3941=COLOUR_RGB('Opaque(154,165,175)', 0.40784314, 0.44705882, 0.49803922);
ENDSEC;
END-ISO-10303-21;
